ISO-10303-21;
HEADER;
FILE_DESCRIPTION (('STEP AP214'),
    '1' );
FILE_NAME ('needle roller bearing_nh_iso_ISO 3245 - 1532D - 14,SI,NC,14.step',
    '2026-10-03T12:29:21',
    ( '' ),
    ( '' ),
    'SwSTEP 2.0',
    'SolidWorks 2026',
    '' );
FILE_SCHEMA (( 'AUTOMOTIVE_DESIGN' ));
ENDSEC;

DATA;
#12=AXIS2_PLACEMENT_3D ( 'NONE', #6697, #8706, #19835 ) ;
#15=ADVANCED_FACE ( 'NONE', ( #19478 ), #14650, .T. ) ;
#41=CARTESIAN_POINT ( 'NONE',  ( -6.165580000000000283, 0.000000000000000000, 0.000000000000000000 ) ) ;
#62=VECTOR ( 'NONE', #8354, 1000.000000000000000 ) ;
#66=ADVANCED_FACE ( 'NONE', ( #13335 ), #6435, .F. ) ;
#87=ORIENTED_EDGE ( 'NONE', *, *, #13366, .F. ) ;
#93=DIRECTION ( 'NONE',  ( -0.000000000000000000, 0.000000000000000000, 1.000000000000000000 ) ) ;
#105=AXIS2_PLACEMENT_3D ( 'NONE', #17790, #10136, #285 ) ;
#151=CIRCLE ( 'NONE', #5555, 10.85999999999999410 ) ;
#158=DIRECTION ( 'NONE',  ( 0.000000000000000000, 0.000000000000000000, -1.000000000000000000 ) ) ;
#159=CARTESIAN_POINT ( 'NONE',  ( 6.165579999999999394, 0.000000000000000000, 0.000000000000000000 ) ) ;
#179=CYLINDRICAL_SURFACE ( 'NONE', #11940, 10.52399999999999380 ) ;
#185=DIRECTION ( 'NONE',  ( 1.000000000000000000, 0.000000000000000000, 0.000000000000000000 ) ) ;
#200=VERTEX_POINT ( 'NONE', #10355 ) ;
#230=MECHANICAL_DESIGN_GEOMETRIC_PRESENTATION_REPRESENTATION('',(#19516),#11670);
#282=DIRECTION ( 'NONE',  ( -1.000000000000000000, -0.000000000000000000, -0.000000000000000000 ) ) ;
#285=DIRECTION ( 'NONE',  ( 0.000000000000000000, 1.000000000000000000, 0.000000000000000000 ) ) ;
#289=ORIENTED_EDGE ( 'NONE', *, *, #11135, .F. ) ;
#292=EDGE_CURVE ( 'NONE', #16213, #10742, #11099, .T. ) ;
#351=ORIENTED_EDGE ( 'NONE', *, *, #3136, .F. ) ;
#352=PRODUCT_DEFINITION_SHAPE ( 'NONE', 'NONE',  #13380 ) ;
#394=ORIENTED_EDGE ( 'NONE', *, *, #20877, .T. ) ;
#430=AXIS2_PLACEMENT_3D ( 'NONE', #20619, #19149, #20718 ) ;
#461=DIRECTION ( 'NONE',  ( -1.836909530733573776E-16, 1.000000000000000000, 0.000000000000000000 ) ) ;
#489=CARTESIAN_POINT ( 'NONE',  ( -31.75000000000000000, 11.49999999999999467, 0.000000000000000000 ) ) ;
#499=FACE_OUTER_BOUND ( 'NONE', #3244, .T. ) ;
#532=CARTESIAN_POINT ( 'NONE',  ( -31.75000000000000000, 0.000000000000000000, 0.000000000000000000 ) ) ;
#581=AXIS2_PLACEMENT_3D ( 'NONE', #14078, #19049, #12260 ) ;
#610=EDGE_LOOP ( 'NONE', ( #11932, #18314, #16602, #14575, #289 ) ) ;
#629=CARTESIAN_POINT ( 'NONE',  ( -7.000000000000000888, 10.52400000000000091, 0.000000000000000000 ) ) ;
#656=DIRECTION ( 'NONE',  ( 0.000000000000000000, 0.000000000000000000, -1.000000000000000000 ) ) ;
#657=ORIENTED_EDGE ( 'NONE', *, *, #4143, .T. ) ;
#665=DIRECTION ( 'NONE',  ( 1.000000000000000000, 1.836909530733573776E-16, 0.000000000000000000 ) ) ;
#698=ADVANCED_FACE ( 'NONE', ( #13281 ), #18053, .T. ) ;
#764=VERTEX_POINT ( 'NONE', #3824 ) ;
#786=CIRCLE ( 'NONE', #7897, 0.06721999999999891950 ) ;
#819=DIRECTION ( 'NONE',  ( -1.000000000000000000, -0.000000000000000000, -0.000000000000000000 ) ) ;
#847=MECHANICAL_DESIGN_GEOMETRIC_PRESENTATION_REPRESENTATION('',(#8628),#6260);
#881=VECTOR ( 'NONE', #12748, 1000.000000000000000 ) ;
#885=ORIENTED_EDGE ( 'NONE', *, *, #18800, .T. ) ;
#905=VECTOR ( 'NONE', #7979, 1000.000000000000000 ) ;
#924=AXIS2_PLACEMENT_3D ( 'NONE', #11112, #6114, #18854 ) ;
#931=AXIS2_PLACEMENT_3D ( 'NONE', #13991, #1176, #17274 ) ;
#935=EDGE_LOOP ( 'NONE', ( #17528, #12852, #4490, #10128 ) ) ;
#1037=VERTEX_POINT ( 'NONE', #19402 ) ;
#1041=DIRECTION ( 'NONE',  ( 1.000000000000000000, 1.836909530733573776E-16, 0.000000000000000000 ) ) ;
#1086=CIRCLE ( 'NONE', #9202, 10.79377999999999993 ) ;
#1146=AXIS2_PLACEMENT_3D ( 'NONE', #18374, #13715, #7032 ) ;
#1150=LINE ( 'NONE', #10570, #2963 ) ;
#1153=CARTESIAN_POINT ( 'NONE',  ( 6.359999999999997655, 7.000462221625649605E-15, 0.000000000000000000 ) ) ;
#1171=ORIENTED_EDGE ( 'NONE', *, *, #13628, .F. ) ;
#1176=DIRECTION ( 'NONE',  ( -2.249565377136137858E-32, 1.224646799147353207E-16, 1.000000000000000000 ) ) ;
#1205=EDGE_CURVE ( 'NONE', #6855, #6330, #4480, .T. ) ;
#1218=CARTESIAN_POINT ( 'NONE',  ( -31.75000000000000000, 0.000000000000000000, 0.000000000000000000 ) ) ;
#1223=DIRECTION ( 'NONE',  ( 0.000000000000000000, -1.224646799147354686E-16, 1.000000000000000000 ) ) ;
#1263=DIRECTION ( 'NONE',  ( -1.000000000000000000, -0.000000000000000000, -0.000000000000000000 ) ) ;
#1279=DIRECTION ( 'NONE',  ( 1.000000000000000000, 1.836909530733573776E-16, 0.000000000000000000 ) ) ;
#1326=DIRECTION ( 'NONE',  ( 1.000000000000000000, 1.836909530733573776E-16, 0.000000000000000000 ) ) ;
#1334=CARTESIAN_POINT ( 'NONE',  ( -6.232800000000000118, 10.79377999999999993, 0.000000000000000000 ) ) ;
#1345=EDGE_CURVE ( 'NONE', #15776, #2254, #12179, .T. ) ;
#1346=EDGE_CURVE ( 'NONE', #14024, #6043, #20389, .T. ) ;
#1393=ORIENTED_EDGE ( 'NONE', *, *, #12307, .F. ) ;
#1430=CARTESIAN_POINT ( 'NONE',  ( -6.165580000000000283, 1.321856812770071588E-15, -10.79377999999999993 ) ) ;
#1453=ORIENTED_EDGE ( 'NONE', *, *, #19628, .T. ) ;
#1461=FACE_OUTER_BOUND ( 'NONE', #9867, .T. ) ;
#1462=TOROIDAL_SURFACE ( 'NONE', #430, 10.79377999999999993, 0.06721999999999977993 ) ;
#1508=FILL_AREA_STYLE_COLOUR ( '', #14117 ) ;
#1561=DIRECTION ( 'NONE',  ( -1.000000000000000000, -0.000000000000000000, -0.000000000000000000 ) ) ;
#1562=EDGE_LOOP ( 'NONE', ( #2821, #6138, #7400, #885, #13620 ) ) ;
#1581=CYLINDRICAL_SURFACE ( 'NONE', #105, 10.52399999999999380 ) ;
#1588=CARTESIAN_POINT ( 'NONE',  ( -6.679999999999998828, 4.605132193549069780E-15, 0.000000000000000000 ) ) ;
#1592=CARTESIAN_POINT ( 'NONE',  ( -31.75000000000000000, 0.000000000000000000, 0.000000000000000000 ) ) ;
#1612=( NAMED_UNIT ( * ) PLANE_ANGLE_UNIT ( ) SI_UNIT ( $, .RADIAN. ) );
#1618=CARTESIAN_POINT ( 'NONE',  ( -6.177131623262581250, 0.000000000000000000, 0.000000000000000000 ) ) ;
#1620=CARTESIAN_POINT ( 'NONE',  ( -31.75000000000000000, 10.85999999999999410, 0.000000000000000000 ) ) ;
#1723=ORIENTED_EDGE ( 'NONE', *, *, #16442, .T. ) ;
#1734=DIRECTION ( 'NONE',  ( -1.000000000000000000, -1.836909530733573776E-16, 0.000000000000000000 ) ) ;
#1740=EDGE_CURVE ( 'NONE', #200, #20371, #6508, .T. ) ;
#1741=DIRECTION ( 'NONE',  ( -1.000000000000000000, -0.000000000000000000, -0.000000000000000000 ) ) ;
#1755=FILL_AREA_STYLE ('',( #3737 ) ) ;
#1814=EDGE_LOOP ( 'NONE', ( #19958, #17807 ) ) ;
#1841=ORIENTED_EDGE ( 'NONE', *, *, #12634, .T. ) ;
#1873=CARTESIAN_POINT ( 'NONE',  ( 6.232799999999996565, 0.000000000000000000, 0.000000000000000000 ) ) ;
#1879=ORIENTED_EDGE ( 'NONE', *, *, #3350, .F. ) ;
#1893=DIRECTION ( 'NONE',  ( -1.000000000000000000, -0.000000000000000000, -0.000000000000000000 ) ) ;
#1901=PLANE ( 'NONE',  #13968 ) ;
#1908=CIRCLE ( 'NONE', #10729, 10.52399999999999380 ) ;
#1914=CIRCLE ( 'NONE', #3599, 11.17999999999999439 ) ;
#1919=CIRCLE ( 'NONE', #4279, 10.52399999999999558 ) ;
#1921=CARTESIAN_POINT ( 'NONE',  ( 6.165579999999996730, 9.184850993605149917E-16, -7.500000000000001776 ) ) ;
#1988=ORIENTED_EDGE ( 'NONE', *, *, #10331, .T. ) ;
#1989=EDGE_CURVE ( 'NONE', #6043, #14024, #14344, .T. ) ;
#2001=ORIENTED_EDGE ( 'NONE', *, *, #13743, .F. ) ;
#2006=DIRECTION ( 'NONE',  ( -1.551631016079434660E-16, 1.000000000000000000, 0.000000000000000000 ) ) ;
#2014=FACE_OUTER_BOUND ( 'NONE', #6061, .T. ) ;
#2037=ORIENTED_EDGE ( 'NONE', *, *, #2248, .F. ) ;
#2049=ORIENTED_EDGE ( 'NONE', *, *, #10414, .T. ) ;
#2074=ORIENTED_EDGE ( 'NONE', *, *, #17740, .F. ) ;
#2096=DIRECTION ( 'NONE',  ( 1.000000000000000000, 1.836909530733573776E-16, 0.000000000000000000 ) ) ;
#2157=AXIS2_PLACEMENT_3D ( 'NONE', #10193, #18573, #656 ) ;
#2182=DIRECTION ( 'NONE',  ( -1.597351267013635531E-16, 1.000000000000000000, 0.000000000000000000 ) ) ;
#2200=EDGE_CURVE ( 'NONE', #4444, #7461, #9248, .T. ) ;
#2210=DIRECTION ( 'NONE',  ( -1.000000000000000000, -1.836909530733573776E-16, 0.000000000000000000 ) ) ;
#2248=EDGE_CURVE ( 'NONE', #20371, #8637, #5954, .T. ) ;
#2252=( GEOMETRIC_REPRESENTATION_CONTEXT ( 3 ) GLOBAL_UNCERTAINTY_ASSIGNED_CONTEXT ( ( #16622 ) ) GLOBAL_UNIT_ASSIGNED_CONTEXT ( ( #20772, #1612, #12630 ) ) REPRESENTATION_CONTEXT ( 'NONE', 'WORKASPACE' ) );
#2254=VERTEX_POINT ( 'NONE', #12326 ) ;
#2325=DIRECTION ( 'NONE',  ( 1.000000000000000000, 1.836909530733573776E-16, 0.000000000000000000 ) ) ;
#2378=EDGE_LOOP ( 'NONE', ( #1879, #14922 ) ) ;
#2384=ORIENTED_EDGE ( 'NONE', *, *, #5532, .F. ) ;
#2415=CARTESIAN_POINT ( 'NONE',  ( -25.39999999999999858, 0.000000000000000000, 0.000000000000000000 ) ) ;
#2458=DIRECTION ( 'NONE',  ( 0.000000000000000000, 0.000000000000000000, 1.000000000000000000 ) ) ;
#2521=VERTEX_POINT ( 'NONE', #14345 ) ;
#2626=AXIS2_PLACEMENT_3D ( 'NONE', #532, #2325, #6979 ) ;
#2738=EDGE_CURVE ( 'NONE', #15842, #6855, #3781, .T. ) ;
#2757=CARTESIAN_POINT ( 'NONE',  ( -6.359999999999999432, 10.85999999999999943, 0.000000000000000000 ) ) ;
#2821=ORIENTED_EDGE ( 'NONE', *, *, #4143, .F. ) ;
#2862=CIRCLE ( 'NONE', #14712, 0.3200000000000017275 ) ;
#2875=FACE_OUTER_BOUND ( 'NONE', #7065, .T. ) ;
#2898=CYLINDRICAL_SURFACE ( 'NONE', #12686, 10.52399999999999558 ) ;
#2918=DIRECTION ( 'NONE',  ( 1.000000000000000000, 1.836909530733573776E-16, 0.000000000000000000 ) ) ;
#2931=ORIENTED_EDGE ( 'NONE', *, *, #2738, .T. ) ;
#2933=CIRCLE ( 'NONE', #4625, 10.85999999999999410 ) ;
#2963=VECTOR ( 'NONE', #1263, 1000.000000000000000 ) ;
#2971=FACE_BOUND ( 'NONE', #19410, .T. ) ;
#2986=ADVANCED_FACE ( 'NONE', ( #19486, #2971 ), #15891, .F. ) ;
#3010=FACE_OUTER_BOUND ( 'NONE', #11793, .T. ) ;
#3014=PLANE ( 'NONE',  #15003 ) ;
#3049=EDGE_LOOP ( 'NONE', ( #15005, #17734, #2074, #19128, #14741 ) ) ;
#3097=DIRECTION ( 'NONE',  ( 1.000000000000000000, 1.836909530733573776E-16, 0.000000000000000000 ) ) ;
#3108=CIRCLE ( 'NONE', #20696, 10.85999999999999410 ) ;
#3136=EDGE_CURVE ( 'NONE', #200, #2521, #7064, .T. ) ;
#3182=DIRECTION ( 'NONE',  ( 1.000000000000000000, 1.836909530733573776E-16, 0.000000000000000000 ) ) ;
#3185=PRESENTATION_STYLE_ASSIGNMENT (( #19093 ) ) ;
#3229=ORIENTED_EDGE ( 'NONE', *, *, #5893, .F. ) ;
#3244=EDGE_LOOP ( 'NONE', ( #2384, #19639, #15365, #13230 ) ) ;
#3274=CARTESIAN_POINT ( 'NONE',  ( -31.75000000000000000, 0.000000000000000000, 0.000000000000000000 ) ) ;
#3311=DIRECTION ( 'NONE',  ( 1.000000000000000000, 1.836909530733573776E-16, 0.000000000000000000 ) ) ;
#3328=DIRECTION ( 'NONE',  ( 1.000000000000000000, 1.836909530733573776E-16, 0.000000000000000000 ) ) ;
#3329=DIRECTION ( 'NONE',  ( 0.000000000000000000, 0.000000000000000000, 1.000000000000000000 ) ) ;
#3350=EDGE_CURVE ( 'NONE', #10983, #18697, #19703, .T. ) ;
#3353=CARTESIAN_POINT ( 'NONE',  ( 6.999999999999999112, 7.118024431592597790E-15, 0.000000000000000000 ) ) ;
#3361=DIRECTION ( 'NONE',  ( 0.000000000000000000, 0.000000000000000000, 1.000000000000000000 ) ) ;
#3363=DIRECTION ( 'NONE',  ( 0.000000000000000000, 1.000000000000000000, 0.000000000000000000 ) ) ;
#3388=EDGE_CURVE ( 'NONE', #5518, #8758, #15995, .T. ) ;
#3434=SURFACE_STYLE_USAGE ( .BOTH. , #16370 ) ;
#3435=DIRECTION ( 'NONE',  ( 0.000000000000000000, 0.000000000000000000, 1.000000000000000000 ) ) ;
#3454=CARTESIAN_POINT ( 'NONE',  ( -31.75000000000000000, 0.000000000000000000, 0.000000000000000000 ) ) ;
#3460=CARTESIAN_POINT ( 'NONE',  ( 6.680000000000000604, 6.938893903907228378E-15, 0.000000000000000000 ) ) ;
#3465=DIRECTION ( 'NONE',  ( 0.000000000000000000, 1.000000000000000000, 0.000000000000000000 ) ) ;
#3477=CARTESIAN_POINT ( 'NONE',  ( 6.679999999999997051, 11.50000000000000178, 0.000000000000000000 ) ) ;
#3525=CARTESIAN_POINT ( 'NONE',  ( -6.359999999999997655, 4.663913298532544267E-15, 0.000000000000000000 ) ) ;
#3588=TOROIDAL_SURFACE ( 'NONE', #8671, 7.567219999999999835, 0.06721999999999891950 ) ;
#3599=AXIS2_PLACEMENT_3D ( 'NONE', #16413, #3182, #2006 ) ;
#3616=CIRCLE ( 'NONE', #581, 10.85999999999999233 ) ;
#3632=DIRECTION ( 'NONE',  ( -2.249565377136137858E-32, 1.224646799147353207E-16, 1.000000000000000000 ) ) ;
#3633=AXIS2_PLACEMENT_3D ( 'NONE', #20403, #4400, #7791 ) ;
#3645=( LENGTH_UNIT ( ) NAMED_UNIT ( * ) SI_UNIT ( .MILLI., .METRE. ) );
#3648=DIRECTION ( 'NONE',  ( 1.000000000000000000, 1.836909530733573776E-16, 0.000000000000000000 ) ) ;
#3651=DIRECTION ( 'NONE',  ( 1.000000000000000000, 1.836909530733573776E-16, 0.000000000000000000 ) ) ;
#3663=ADVANCED_FACE ( 'NONE', ( #9521 ), #9815, .T. ) ;
#3665=PRODUCT_CONTEXT ( 'NONE', #18324, 'mechanical' ) ;
#3685=DIRECTION ( 'NONE',  ( 1.000000000000000000, 0.000000000000000000, 0.000000000000000000 ) ) ;
#3737=FILL_AREA_STYLE_COLOUR ( '', #10997 ) ;
#3781=CIRCLE ( 'NONE', #16652, 0.3200000000000008393 ) ;
#3805=CARTESIAN_POINT ( 'NONE',  ( -6.165580000000000283, 0.000000000000000000, 0.000000000000000000 ) ) ;
#3824=CARTESIAN_POINT ( 'NONE',  ( 6.177131623262577698, 10.85999999999999410, 0.000000000000000000 ) ) ;
#3870=ORIENTED_EDGE ( 'NONE', *, *, #6122, .F. ) ;
#3871=CIRCLE ( 'NONE', #19139, 10.52399999999999558 ) ;
#3962=DIRECTION ( 'NONE',  ( -1.000000000000000000, -0.000000000000000000, -0.000000000000000000 ) ) ;
#3991=VERTEX_POINT ( 'NONE', #13086 ) ;
#4008=CARTESIAN_POINT ( 'NONE',  ( -6.359999999999997655, 4.663913298532544267E-15, 0.000000000000000000 ) ) ;
#4054=ORIENTED_EDGE ( 'NONE', *, *, #2200, .T. ) ;
#4084=CIRCLE ( 'NONE', #12565, 11.49999999999999467 ) ;
#4113=VECTOR ( 'NONE', #2918, 1000.000000000000000 ) ;
#4143=EDGE_CURVE ( 'NONE', #6043, #11637, #20263, .T. ) ;
#4177=EDGE_LOOP ( 'NONE', ( #10550, #12157 ) ) ;
#4195=CYLINDRICAL_SURFACE ( 'NONE', #4491, 7.500000000000000000 ) ;
#4214=DIRECTION ( 'NONE',  ( 0.000000000000000000, 1.000000000000000000, 0.000000000000000000 ) ) ;
#4240=DIRECTION ( 'NONE',  ( -1.508455196501572169E-16, 1.000000000000000000, 0.000000000000000000 ) ) ;
#4245=CARTESIAN_POINT ( 'NONE',  ( 6.177131623262577698, 0.000000000000000000, 0.000000000000000000 ) ) ;
#4270=ORIENTED_EDGE ( 'NONE', *, *, #20114, .T. ) ;
#4279=AXIS2_PLACEMENT_3D ( 'NONE', #7781, #12674, #14055 ) ;
#4289=CARTESIAN_POINT ( 'NONE',  ( 6.177131623262577698, 0.000000000000000000, 0.000000000000000000 ) ) ;
#4316=CIRCLE ( 'NONE', #931, 0.3200000000000008393 ) ;
#4343=CARTESIAN_POINT ( 'NONE',  ( -6.232800000000000118, 9.267171751443831555E-16, -7.567219999999999835 ) ) ;
#4353=ORIENTED_EDGE ( 'NONE', *, *, #19178, .F. ) ;
#4382=ORIENTED_EDGE ( 'NONE', *, *, #4753, .F. ) ;
#4400=DIRECTION ( 'NONE',  ( -1.000000000000000000, -0.000000000000000000, -0.000000000000000000 ) ) ;
#4444=VERTEX_POINT ( 'NONE', #1921 ) ;
#4464=DIRECTION ( 'NONE',  ( 0.000000000000000000, -1.000000000000000000, 0.000000000000000000 ) ) ;
#4465=EDGE_LOOP ( 'NONE', ( #1723, #19275, #11473, #11086 ) ) ;
#4480=CIRCLE ( 'NONE', #11585, 11.17999999999999261 ) ;
#4490=ORIENTED_EDGE ( 'NONE', *, *, #13743, .T. ) ;
#4491=AXIS2_PLACEMENT_3D ( 'NONE', #15325, #16914, #7369 ) ;
#4505=LINE ( 'NONE', #4717, #4113 ) ;
#4567=( NAMED_UNIT ( * ) PLANE_ANGLE_UNIT ( ) SI_UNIT ( $, .RADIAN. ) );
#4584=ORIENTED_EDGE ( 'NONE', *, *, #1345, .F. ) ;
#4590=ADVANCED_FACE ( 'NONE', ( #20129 ), #12579, .T. ) ;
#4622=CIRCLE ( 'NONE', #18511, 7.500000000000000000 ) ;
#4625=AXIS2_PLACEMENT_3D ( 'NONE', #19494, #3685, #13353 ) ;
#4627=DIRECTION ( 'NONE',  ( 1.000000000000000000, 1.836909530733573776E-16, 0.000000000000000000 ) ) ;
#4702=EDGE_CURVE ( 'NONE', #15842, #2254, #4084, .T. ) ;
#4717=CARTESIAN_POINT ( 'NONE',  ( -31.75000000000000000, -10.52399999999999380, 1.288818291422673781E-15 ) ) ;
#4753=EDGE_CURVE ( 'NONE', #4894, #3991, #1086, .T. ) ;
#4760=LINE ( 'NONE', #16110, #62 ) ;
#4790=DIRECTION ( 'NONE',  ( 1.000000000000000000, 1.836909530733573776E-16, 0.000000000000000000 ) ) ;
#4792=EDGE_CURVE ( 'NONE', #7461, #1037, #4760, .T. ) ;
#4857=DIRECTION ( 'NONE',  ( 1.000000000000000000, 1.836909530733573776E-16, 0.000000000000000000 ) ) ;
#4894=VERTEX_POINT ( 'NONE', #8145 ) ;
#4908=DIRECTION ( 'NONE',  ( 1.836909530733573776E-16, -1.000000000000000000, 0.000000000000000000 ) ) ;
#4930=CARTESIAN_POINT ( 'NONE',  ( 6.232799999999996565, 0.000000000000000000, 0.000000000000000000 ) ) ;
#4952=DIRECTION ( 'NONE',  ( 0.000000000000000000, 1.000000000000000000, 0.000000000000000000 ) ) ;
#4959=CIRCLE ( 'NONE', #7324, 10.79377999999999993 ) ;
#4967=TOROIDAL_SURFACE ( 'NONE', #19522, 7.567219999999999835, 0.06721999999999891950 ) ;
#4971=DIRECTION ( 'NONE',  ( -1.000000000000000000, 0.000000000000000000, -0.000000000000000000 ) ) ;
#4991=DIRECTION ( 'NONE',  ( 1.000000000000000000, 0.000000000000000000, 0.000000000000000000 ) ) ;
#5005=AXIS2_PLACEMENT_3D ( 'NONE', #5230, #3632, #14504 ) ;
#5008=TOROIDAL_SURFACE ( 'NONE', #3633, 10.79377999999999993, 0.06721999999999934972 ) ;
#5052=ADVANCED_FACE ( 'NONE', ( #16721 ), #8660, .F. ) ;
#5069=EDGE_CURVE ( 'NONE', #16213, #14635, #12242, .T. ) ;
#5121=TOROIDAL_SURFACE ( 'NONE', #14959, 10.79377999999999993, 0.06721999999999977993 ) ;
#5130=FACE_OUTER_BOUND ( 'NONE', #610, .T. ) ;
#5146=VECTOR ( 'NONE', #2096, 1000.000000000000000 ) ;
#5213=AXIS2_PLACEMENT_3D ( 'NONE', #5224, #19432, #3329 ) ;
#5224=CARTESIAN_POINT ( 'NONE',  ( -6.232800000000000118, 0.000000000000000000, 0.000000000000000000 ) ) ;
#5230=CARTESIAN_POINT ( 'NONE',  ( -6.679999999999996163, -11.17999999999998906, 1.369155121446740171E-15 ) ) ;
#5325=CIRCLE ( 'NONE', #5005, 0.3200000000000008393 ) ;
#5336=EDGE_CURVE ( 'NONE', #8404, #13162, #18465, .T. ) ;
#5345=CYLINDRICAL_SURFACE ( 'NONE', #9808, 10.85999999999999410 ) ;
#5359=CARTESIAN_POINT ( 'NONE',  ( 6.359999999999995879, 10.85999999999999943, 0.000000000000000000 ) ) ;
#5381=LINE ( 'NONE', #10267, #9710 ) ;
#5384=UNCERTAINTY_MEASURE_WITH_UNIT (LENGTH_MEASURE( 1.000000000000000082E-05 ), #6360, 'distance_accuracy_value', 'NONE');
#5385=DIRECTION ( 'NONE',  ( 1.000000000000000000, 1.836909530733573776E-16, 0.000000000000000000 ) ) ;
#5442=DIRECTION ( 'NONE',  ( -1.648349939164583742E-16, 1.000000000000000000, 0.000000000000000000 ) ) ;
#5488=AXIS2_PLACEMENT_3D ( 'NONE', #7460, #11082, #17121 ) ;
#5518=VERTEX_POINT ( 'NONE', #6383 ) ;
#5532=EDGE_CURVE ( 'NONE', #14635, #16213, #14430, .T. ) ;
#5554=ORIENTED_EDGE ( 'NONE', *, *, #16443, .F. ) ;
#5555=AXIS2_PLACEMENT_3D ( 'NONE', #17303, #15499, #7758 ) ;
#5559=DIRECTION ( 'NONE',  ( 0.000000000000000000, -1.224646799147341867E-16, 1.000000000000000000 ) ) ;
#5605=ORIENTED_EDGE ( 'NONE', *, *, #9023, .T. ) ;
#5751=ORIENTED_EDGE ( 'NONE', *, *, #14798, .T. ) ;
#5765=AXIS2_PLACEMENT_3D ( 'NONE', #19531, #1734, #4908 ) ;
#5800=CYLINDRICAL_SURFACE ( 'NONE', #13436, 7.500000000000000000 ) ;
#5825=ORIENTED_EDGE ( 'NONE', *, *, #11135, .T. ) ;
#5826=EDGE_LOOP ( 'NONE', ( #5554, #4382 ) ) ;
#5852=EDGE_LOOP ( 'NONE', ( #8337, #9933, #12486, #2037 ) ) ;
#5893=EDGE_CURVE ( 'NONE', #18535, #17067, #5968, .T. ) ;
#5927=AXIS2_PLACEMENT_3D ( 'NONE', #18177, #6611, #158 ) ;
#5938=ORIENTED_EDGE ( 'NONE', *, *, #4702, .F. ) ;
#5954=LINE ( 'NONE', #12433, #19422 ) ;
#5967=DIRECTION ( 'NONE',  ( 0.000000000000000000, 1.000000000000000000, 0.000000000000000000 ) ) ;
#5968=CIRCLE ( 'NONE', #6968, 10.85999999999999410 ) ;
#6017=DIRECTION ( 'NONE',  ( 1.000000000000000000, 1.836909530733573776E-16, 0.000000000000000000 ) ) ;
#6021=ORIENTED_EDGE ( 'NONE', *, *, #5069, .T. ) ;
#6023=AXIS2_PLACEMENT_3D ( 'NONE', #1588, #4857, #11327 ) ;
#6029=FACE_OUTER_BOUND ( 'NONE', #4177, .T. ) ;
#6040=ORIENTED_EDGE ( 'NONE', *, *, #19319, .T. ) ;
#6043=VERTEX_POINT ( 'NONE', #9535 ) ;
#6061=EDGE_LOOP ( 'NONE', ( #394, #8047, #5938, #9208 ) ) ;
#6076=DIRECTION ( 'NONE',  ( 0.000000000000000000, -1.224646799147354686E-16, 1.000000000000000000 ) ) ;
#6088=ORIENTED_EDGE ( 'NONE', *, *, #4753, .T. ) ;
#6114=DIRECTION ( 'NONE',  ( 1.000000000000000000, 1.836909530733573776E-16, 0.000000000000000000 ) ) ;
#6122=EDGE_CURVE ( 'NONE', #18991, #12032, #7319, .T. ) ;
#6131=ADVANCED_BREP_SHAPE_REPRESENTATION ( '', ( #10450, #12461 ), #2252 ) ;
#6138=ORIENTED_EDGE ( 'NONE', *, *, #1346, .F. ) ;
#6165=CARTESIAN_POINT ( 'NONE',  ( -31.75000000000000000, -10.85999999999999410, 1.329966423874024955E-15 ) ) ;
#6195=EDGE_CURVE ( 'NONE', #18697, #10983, #1914, .T. ) ;
#6201=AXIS2_PLACEMENT_3D ( 'NONE', #3525, #16460, #17757 ) ;
#6224=DIRECTION ( 'NONE',  ( -1.000000000000000000, -0.000000000000000000, -0.000000000000000000 ) ) ;
#6231=CIRCLE ( 'NONE', #5213, 7.567219999999999835 ) ;
#6260=( GEOMETRIC_REPRESENTATION_CONTEXT ( 3 ) GLOBAL_UNCERTAINTY_ASSIGNED_CONTEXT ( ( #13462 ) ) GLOBAL_UNIT_ASSIGNED_CONTEXT ( ( #3645, #10218, #13414 ) ) REPRESENTATION_CONTEXT ( 'NONE', 'WORKASPACE' ) );
#6262=DIRECTION ( 'NONE',  ( 1.000000000000000000, 0.000000000000000000, 0.000000000000000000 ) ) ;
#6287=AXIS2_PLACEMENT_3D ( 'NONE', #1873, #282, #8329 ) ;
#6297=EDGE_LOOP ( 'NONE', ( #12035, #19587, #11065, #5751, #20058 ) ) ;
#6304=AXIS2_PLACEMENT_3D ( 'NONE', #6724, #10227, #15001 ) ;
#6328=DIRECTION ( 'NONE',  ( 1.000000000000000000, 1.836909530733573776E-16, 0.000000000000000000 ) ) ;
#6330=VERTEX_POINT ( 'NONE', #7389 ) ;
#6333=CIRCLE ( 'NONE', #13467, 0.06721999999999891950 ) ;
#6360=( LENGTH_UNIT ( ) NAMED_UNIT ( * ) SI_UNIT ( .MILLI., .METRE. ) );
#6383=CARTESIAN_POINT ( 'NONE',  ( 6.359999999999999432, -10.85999999999998522, 1.329966423874024758E-15 ) ) ;
#6411=ORIENTED_EDGE ( 'NONE', *, *, #13134, .F. ) ;
#6435=CYLINDRICAL_SURFACE ( 'NONE', #16670, 10.52399999999999558 ) ;
#6441=EDGE_LOOP ( 'NONE', ( #20606, #19757, #14209, #9585 ) ) ;
#6453=( NAMED_UNIT ( * ) SI_UNIT ( $, .STERADIAN. ) SOLID_ANGLE_UNIT ( ) );
#6508=CIRCLE ( 'NONE', #5488, 10.52399999999999558 ) ;
#6526=EDGE_CURVE ( 'NONE', #2254, #15842, #6661, .T. ) ;
#6543=DIRECTION ( 'NONE',  ( 1.000000000000000000, 1.836909530733573776E-16, 0.000000000000000000 ) ) ;
#6549=AXIS2_PLACEMENT_3D ( 'NONE', #12281, #1279, #9517 ) ;
#6585=CARTESIAN_POINT ( 'NONE',  ( 6.232799999999996565, 0.000000000000000000, 0.000000000000000000 ) ) ;
#6608=CARTESIAN_POINT ( 'NONE',  ( 7.000000000000000888, -10.52399999999998670, 1.288818291422673781E-15 ) ) ;
#6611=DIRECTION ( 'NONE',  ( 0.000000000000000000, -1.000000000000000000, 0.000000000000000000 ) ) ;
#6632=EDGE_LOOP ( 'NONE', ( #87, #11751, #1841, #4353 ) ) ;
#6645=CIRCLE ( 'NONE', #18508, 10.52399999999999558 ) ;
#6661=CIRCLE ( 'NONE', #924, 11.49999999999999467 ) ;
#6677=AXIS2_PLACEMENT_3D ( 'NONE', #4289, #3962, #18496 ) ;
#6697=CARTESIAN_POINT ( 'NONE',  ( -6.232800000000000118, 0.000000000000000000, 0.000000000000000000 ) ) ;
#6721=CARTESIAN_POINT ( 'NONE',  ( -31.75000000000000000, 0.000000000000000000, 0.000000000000000000 ) ) ;
#6724=CARTESIAN_POINT ( 'NONE',  ( -6.679999999999998828, 4.605132193549069780E-15, 0.000000000000000000 ) ) ;
#6778=ORIENTED_EDGE ( 'NONE', *, *, #19207, .T. ) ;
#6821=ORIENTED_EDGE ( 'NONE', *, *, #20114, .F. ) ;
#6825=CARTESIAN_POINT ( 'NONE',  ( -6.177131623262581250, 1.329966423874024758E-15, -10.85999999999999410 ) ) ;
#6838=AXIS2_PLACEMENT_3D ( 'NONE', #18192, #10132, #2182 ) ;
#6854=EDGE_CURVE ( 'NONE', #4444, #13162, #6333, .T. ) ;
#6855=VERTEX_POINT ( 'NONE', #12036 ) ;
#6899=AXIS2_PLACEMENT_3D ( 'NONE', #19448, #19247, #3435 ) ;
#6902=CARTESIAN_POINT ( 'NONE',  ( 6.177131623262577698, -10.85999999999999410, 1.329966423874025941E-15 ) ) ;
#6915=ORIENTED_EDGE ( 'NONE', *, *, #6526, .F. ) ;
#6923=CARTESIAN_POINT ( 'NONE',  ( -6.232800000000000118, 0.000000000000000000, 0.000000000000000000 ) ) ;
#6938=CARTESIAN_POINT ( 'NONE',  ( -6.999999999999997335, 10.52400000000000091, 0.000000000000000000 ) ) ;
#6944=ADVANCED_FACE ( 'NONE', ( #18716 ), #5008, .T. ) ;
#6956=CIRCLE ( 'NONE', #19160, 0.06721999999999977993 ) ;
#6968=AXIS2_PLACEMENT_3D ( 'NONE', #4245, #11985, #18659 ) ;
#6974=CARTESIAN_POINT ( 'NONE',  ( 6.999999999999999112, 7.118024431592597790E-15, 0.000000000000000000 ) ) ;
#6979=DIRECTION ( 'NONE',  ( 0.000000000000000000, 1.000000000000000000, 0.000000000000000000 ) ) ;
#6984=AXIS2_PLACEMENT_3D ( 'NONE', #11234, #17709, #12937 ) ;
#6990=DIRECTION ( 'NONE',  ( 0.000000000000000000, 0.000000000000000000, -1.000000000000000000 ) ) ;
#7032=DIRECTION ( 'NONE',  ( -1.836909530733573776E-16, 1.000000000000000000, 0.000000000000000000 ) ) ;
#7034=EDGE_LOOP ( 'NONE', ( #15914, #12439 ) ) ;
#7064=LINE ( 'NONE', #16607, #5146 ) ;
#7065=EDGE_LOOP ( 'NONE', ( #18824, #13673, #18055, #17857, #16663 ) ) ;
#7128=EDGE_LOOP ( 'NONE', ( #18033, #6088, #2049, #9113, #3229 ) ) ;
#7148=CARTESIAN_POINT ( 'NONE',  ( 6.165580000000000283, 9.267171751443833528E-16, -7.567219999999999835 ) ) ;
#7197=DIRECTION ( 'NONE',  ( -1.000000000000000000, -0.000000000000000000, -0.000000000000000000 ) ) ;
#7233=FACE_OUTER_BOUND ( 'NONE', #18715, .T. ) ;
#7285=DIRECTION ( 'NONE',  ( 0.000000000000000000, 0.000000000000000000, 1.000000000000000000 ) ) ;
#7319=CIRCLE ( 'NONE', #6984, 0.06721999999999977993 ) ;
#7324=AXIS2_PLACEMENT_3D ( 'NONE', #14769, #1741, #8195 ) ;
#7346=CIRCLE ( 'NONE', #17853, 10.85999999999999410 ) ;
#7369=DIRECTION ( 'NONE',  ( 0.000000000000000000, 0.000000000000000000, 1.000000000000000000 ) ) ;
#7389=CARTESIAN_POINT ( 'NONE',  ( 7.000000000000000888, -11.17999999999998550, 1.388749470233097582E-15 ) ) ;
#7400=ORIENTED_EDGE ( 'NONE', *, *, #7693, .T. ) ;
#7460=CARTESIAN_POINT ( 'NONE',  ( -6.999999999999995559, 4.546351088565595293E-15, 0.000000000000000000 ) ) ;
#7461=VERTEX_POINT ( 'NONE', #8151 ) ;
#7497=AXIS2_PLACEMENT_3D ( 'NONE', #1153, #1041, #20633 ) ;
#7520=ORIENTED_EDGE ( 'NONE', *, *, #14376, .F. ) ;
#7524=VECTOR ( 'NONE', #10489, 1000.000000000000000 ) ;
#7528=EDGE_CURVE ( 'NONE', #19132, #14670, #2933, .T. ) ;
#7549=CARTESIAN_POINT ( 'NONE',  ( -6.165580000000000283, 0.000000000000000000, 0.000000000000000000 ) ) ;
#7691=ADVANCED_FACE ( 'NONE', ( #19905 ), #5800, .F. ) ;
#7693=EDGE_CURVE ( 'NONE', #14024, #14670, #5381, .T. ) ;
#7699=CIRCLE ( 'NONE', #10068, 10.85999999999999410 ) ;
#7751=DIRECTION ( 'NONE',  ( 0.000000000000000000, 0.000000000000000000, 1.000000000000000000 ) ) ;
#7758=DIRECTION ( 'NONE',  ( 0.000000000000000000, 0.000000000000000000, 1.000000000000000000 ) ) ;
#7775=ORIENTED_EDGE ( 'NONE', *, *, #9754, .T. ) ;
#7781=CARTESIAN_POINT ( 'NONE',  ( -6.999999999999995559, 4.546351088565595293E-15, 0.000000000000000000 ) ) ;
#7791=DIRECTION ( 'NONE',  ( 0.000000000000000000, 0.000000000000000000, 1.000000000000000000 ) ) ;
#7874=FACE_OUTER_BOUND ( 'NONE', #14113, .T. ) ;
#7880=DIRECTION ( 'NONE',  ( -0.000000000000000000, 1.000000000000000000, 1.224646799147353207E-16 ) ) ;
#7897=AXIS2_PLACEMENT_3D ( 'NONE', #19144, #18934, #17657 ) ;
#7922=PLANE ( 'NONE',  #20741 ) ;
#7926=CIRCLE ( 'NONE', #6899, 7.500000000000000888 ) ;
#7958=SURFACE_SIDE_STYLE ('',( #17818 ) ) ;
#7970=ORIENTED_EDGE ( 'NONE', *, *, #2738, .F. ) ;
#7979=DIRECTION ( 'NONE',  ( 1.000000000000000000, 1.836909530733573776E-16, 0.000000000000000000 ) ) ;
#8012=AXIS2_PLACEMENT_3D ( 'NONE', #17840, #3311, #9773 ) ;
#8047=ORIENTED_EDGE ( 'NONE', *, *, #1345, .T. ) ;
#8112=CARTESIAN_POINT ( 'NONE',  ( -6.359999999999997655, 4.663913298532544267E-15, 0.000000000000000000 ) ) ;
#8145=CARTESIAN_POINT ( 'NONE',  ( 6.232799999999996565, 1.325911618322048272E-15, -10.79377999999999993 ) ) ;
#8151=CARTESIAN_POINT ( 'NONE',  ( 6.165579999999996730, 0.000000000000000000, 7.500000000000000888 ) ) ;
#8157=EDGE_CURVE ( 'NONE', #14635, #9288, #4505, .T. ) ;
#8195=DIRECTION ( 'NONE',  ( 0.000000000000000000, 0.000000000000000000, 1.000000000000000000 ) ) ;
#8221=EDGE_LOOP ( 'NONE', ( #12856, #18052 ) ) ;
#8240=ADVANCED_FACE ( 'NONE', ( #16616, #19694 ), #1901, .T. ) ;
#8329=DIRECTION ( 'NONE',  ( 0.000000000000000000, 0.000000000000000000, 1.000000000000000000 ) ) ;
#8337=ORIENTED_EDGE ( 'NONE', *, *, #1740, .F. ) ;
#8345=DIRECTION ( 'NONE',  ( 1.000000000000000000, 1.836909530733573776E-16, 0.000000000000000000 ) ) ;
#8354=DIRECTION ( 'NONE',  ( -1.000000000000000000, -0.000000000000000000, -0.000000000000000000 ) ) ;
#8404=VERTEX_POINT ( 'NONE', #18541 ) ;
#8418=ORIENTED_EDGE ( 'NONE', *, *, #6854, .F. ) ;
#8491=ORIENTED_EDGE ( 'NONE', *, *, #7528, .T. ) ;
#8514=EDGE_LOOP ( 'NONE', ( #3870, #15057, #13010, #2001 ) ) ;
#8577=CIRCLE ( 'NONE', #20434, 0.06721999999999977993 ) ;
#8589=DIRECTION ( 'NONE',  ( 0.000000000000000000, 0.000000000000000000, 1.000000000000000000 ) ) ;
#8628=STYLED_ITEM ( 'NONE', ( #11600 ), #10450 ) ;
#8637=VERTEX_POINT ( 'NONE', #9514 ) ;
#8660=CYLINDRICAL_SURFACE ( 'NONE', #15960, 10.85999999999999410 ) ;
#8671=AXIS2_PLACEMENT_3D ( 'NONE', #15961, #14074, #17462 ) ;
#8680=ADVANCED_FACE ( 'NONE', ( #14406 ), #1581, .F. ) ;
#8706=DIRECTION ( 'NONE',  ( -1.000000000000000000, -0.000000000000000000, -0.000000000000000000 ) ) ;
#8719=DIRECTION ( 'NONE',  ( -1.000000000000000000, -0.000000000000000000, -0.000000000000000000 ) ) ;
#8722=CARTESIAN_POINT ( 'NONE',  ( -31.75000000000000000, -10.85999999999999410, 1.329966423874024955E-15 ) ) ;
#8733=ADVANCED_FACE ( 'NONE', ( #499 ), #179, .F. ) ;
#8754=CARTESIAN_POINT ( 'NONE',  ( 6.177131623262577698, 0.000000000000000000, 10.85999999999999410 ) ) ;
#8758=VERTEX_POINT ( 'NONE', #5359 ) ;
#8780=DIRECTION ( 'NONE',  ( 1.000000000000000000, 1.836909530733573776E-16, 0.000000000000000000 ) ) ;
#8811=PRODUCT ( 'needle roller bearing_nh_iso_ISO 3245 - 1532D - 14,SI,NC,14', 'needle roller bearing_nh_iso_ISO 3245 - 1532D - 14,SI,NC,14', '', ( #3665 ) ) ;
#8827=ADVANCED_FACE ( 'NONE', ( #10347 ), #4195, .F. ) ;
#8876=DIRECTION ( 'NONE',  ( -1.000000000000000000, -0.000000000000000000, -0.000000000000000000 ) ) ;
#8924=ORIENTED_EDGE ( 'NONE', *, *, #10272, .F. ) ;
#9023=EDGE_CURVE ( 'NONE', #7461, #8404, #786, .T. ) ;
#9034=AXIS2_PLACEMENT_3D ( 'NONE', #18157, #3328, #461 ) ;
#9107=PLANE ( 'NONE',  #6549 ) ;
#9113=ORIENTED_EDGE ( 'NONE', *, *, #12362, .F. ) ;
#9120=DIRECTION ( 'NONE',  ( 1.000000000000000000, 1.836909530733573776E-16, 0.000000000000000000 ) ) ;
#9202=AXIS2_PLACEMENT_3D ( 'NONE', #9836, #1893, #11638 ) ;
#9208=ORIENTED_EDGE ( 'NONE', *, *, #19207, .F. ) ;
#9243=ORIENTED_EDGE ( 'NONE', *, *, #12362, .T. ) ;
#9248=CIRCLE ( 'NONE', #10270, 7.500000000000000888 ) ;
#9266=CARTESIAN_POINT ( 'NONE',  ( 6.165579999999999394, 1.321856812770071588E-15, -10.79377999999999993 ) ) ;
#9288=VERTEX_POINT ( 'NONE', #6608 ) ;
#9304=ORIENTED_EDGE ( 'NONE', *, *, #16442, .F. ) ;
#9341=CARTESIAN_POINT ( 'NONE',  ( -6.165580000000000283, 0.000000000000000000, 0.000000000000000000 ) ) ;
#9350=ADVANCED_FACE ( 'NONE', ( #7233 ), #10614, .T. ) ;
#9360=CARTESIAN_POINT ( 'NONE',  ( 6.359999999999997655, 7.000462221625649605E-15, 0.000000000000000000 ) ) ;
#9387=ORIENTED_EDGE ( 'NONE', *, *, #20877, .F. ) ;
#9459=DIRECTION ( 'NONE',  ( -1.000000000000000000, -0.000000000000000000, -0.000000000000000000 ) ) ;
#9509=FACE_OUTER_BOUND ( 'NONE', #8221, .T. ) ;
#9514=CARTESIAN_POINT ( 'NONE',  ( -6.359999999999999432, 10.52400000000000091, 0.000000000000000000 ) ) ;
#9517=DIRECTION ( 'NONE',  ( -1.836909530733573776E-16, 1.000000000000000000, 0.000000000000000000 ) ) ;
#9521=FACE_OUTER_BOUND ( 'NONE', #6632, .T. ) ;
#9535=CARTESIAN_POINT ( 'NONE',  ( -6.359999999999995879, -10.85999999999998877, 1.329966423874024955E-15 ) ) ;
#9545=DIRECTION ( 'NONE',  ( 0.000000000000000000, 0.000000000000000000, -1.000000000000000000 ) ) ;
#9584=CARTESIAN_POINT ( 'NONE',  ( -6.165580000000000283, 9.226011372524489750E-16, -7.500000000000000000 ) ) ;
#9585=ORIENTED_EDGE ( 'NONE', *, *, #13628, .T. ) ;
#9598=DIRECTION ( 'NONE',  ( 1.000000000000000000, 1.836909530733573776E-16, 0.000000000000000000 ) ) ;
#9620=DIRECTION ( 'NONE',  ( -1.648349939164583989E-16, 1.000000000000000000, 0.000000000000000000 ) ) ;
#9677=AXIS2_PLACEMENT_3D ( 'NONE', #9266, #15929, #1223 ) ;
#9710=VECTOR ( 'NONE', #16839, 1000.000000000000000 ) ;
#9754=EDGE_CURVE ( 'NONE', #13162, #8404, #20439, .T. ) ;
#9773=DIRECTION ( 'NONE',  ( 0.000000000000000000, 1.000000000000000000, 0.000000000000000000 ) ) ;
#9783=FACE_BOUND ( 'NONE', #19182, .T. ) ;
#9808=AXIS2_PLACEMENT_3D ( 'NONE', #6721, #3648, #11604 ) ;
#9815=TOROIDAL_SURFACE ( 'NONE', #20648, 11.17999999999999439, 0.3200000000000012834 ) ;
#9836=CARTESIAN_POINT ( 'NONE',  ( 6.232799999999996565, 0.000000000000000000, 0.000000000000000000 ) ) ;
#9867=EDGE_LOOP ( 'NONE', ( #8418, #4054, #5605, #20311 ) ) ;
#9895=CLOSED_SHELL ( 'NONE', ( #17327, #16546, #13892, #8827, #4590, #8733, #9350, #18946, #19651, #66, #19818, #17820, #13873, #5052, #14350, #15058, #8240, #3663, #698, #15, #15944, #8680, #16991, #13337, #7691, #11535, #2986, #6944, #16320, #14403 ) ) ;
#9933=ORIENTED_EDGE ( 'NONE', *, *, #3136, .T. ) ;
#9938=ORIENTED_EDGE ( 'NONE', *, *, #1205, .F. ) ;
#9968=CYLINDRICAL_SURFACE ( 'NONE', #8012, 10.85999999999999410 ) ;
#9996=CIRCLE ( 'NONE', #9677, 0.06721999999999977993 ) ;
#9999=DIRECTION ( 'NONE',  ( -1.000000000000000000, -0.000000000000000000, -0.000000000000000000 ) ) ;
#10068=AXIS2_PLACEMENT_3D ( 'NONE', #17492, #15477, #14314 ) ;
#10128=ORIENTED_EDGE ( 'NONE', *, *, #4792, .F. ) ;
#10132=DIRECTION ( 'NONE',  ( 1.000000000000000000, 1.836909530733573776E-16, 0.000000000000000000 ) ) ;
#10136=DIRECTION ( 'NONE',  ( 1.000000000000000000, 1.836909530733573776E-16, 0.000000000000000000 ) ) ;
#10193=CARTESIAN_POINT ( 'NONE',  ( -6.165580000000000283, 0.000000000000000000, 10.79377999999999993 ) ) ;
#10218=( NAMED_UNIT ( * ) PLANE_ANGLE_UNIT ( ) SI_UNIT ( $, .RADIAN. ) );
#10227=DIRECTION ( 'NONE',  ( 1.000000000000000000, 1.836909530733573776E-16, 0.000000000000000000 ) ) ;
#10258=VERTEX_POINT ( 'NONE', #16623 ) ;
#10267=CARTESIAN_POINT ( 'NONE',  ( -31.75000000000000000, 10.85999999999999410, 0.000000000000000000 ) ) ;
#10270=AXIS2_PLACEMENT_3D ( 'NONE', #10314, #8719, #16665 ) ;
#10272=EDGE_CURVE ( 'NONE', #6330, #6855, #13710, .T. ) ;
#10290=DIRECTION ( 'NONE',  ( -1.000000000000000000, -0.000000000000000000, -0.000000000000000000 ) ) ;
#10314=CARTESIAN_POINT ( 'NONE',  ( 6.165579999999996730, 0.000000000000000000, 0.000000000000000000 ) ) ;
#10331=EDGE_CURVE ( 'NONE', #8637, #2521, #3871, .T. ) ;
#10347=FACE_OUTER_BOUND ( 'NONE', #935, .T. ) ;
#10355=CARTESIAN_POINT ( 'NONE',  ( -6.999999999999993783, -10.52399999999999025, 1.288818291422673979E-15 ) ) ;
#10391=EDGE_LOOP ( 'NONE', ( #17533, #657, #19086, #8491, #16583 ) ) ;
#10414=EDGE_CURVE ( 'NONE', #3991, #16258, #13382, .T. ) ;
#10443=DIRECTION ( 'NONE',  ( 1.000000000000000000, 1.836909530733573776E-16, 0.000000000000000000 ) ) ;
#10450=MANIFOLD_SOLID_BREP ( 'RollersSimplified', #9895 ) ;
#10489=DIRECTION ( 'NONE',  ( 1.000000000000000000, 1.836909530733573776E-16, 0.000000000000000000 ) ) ;
#10550=ORIENTED_EDGE ( 'NONE', *, *, #1205, .T. ) ;
#10561=CARTESIAN_POINT ( 'NONE',  ( 6.359999999999995879, 10.52400000000000091, 0.000000000000000000 ) ) ;
#10570=CARTESIAN_POINT ( 'NONE',  ( -25.39999999999999858, 9.184850993605147944E-16, -7.500000000000000000 ) ) ;
#10614=TOROIDAL_SURFACE ( 'NONE', #1146, 11.17999999999999261, 0.3200000000000008393 ) ;
#10637=EDGE_CURVE ( 'NONE', #4894, #18535, #9996, .T. ) ;
#10665=VERTEX_POINT ( 'NONE', #20911 ) ;
#10702=AXIS2_PLACEMENT_3D ( 'NONE', #9360, #4790, #19005 ) ;
#10729=AXIS2_PLACEMENT_3D ( 'NONE', #20682, #3097, #10746 ) ;
#10742=VERTEX_POINT ( 'NONE', #18045 ) ;
#10746=DIRECTION ( 'NONE',  ( -1.648349939164583989E-16, 1.000000000000000000, 0.000000000000000000 ) ) ;
#10812=DIRECTION ( 'NONE',  ( 1.000000000000000000, 1.836909530733573776E-16, 0.000000000000000000 ) ) ;
#10836=DIRECTION ( 'NONE',  ( 1.000000000000000000, 1.836909530733573776E-16, 0.000000000000000000 ) ) ;
#10840=LINE ( 'NONE', #6165, #905 ) ;
#10958=EDGE_CURVE ( 'NONE', #14005, #1037, #6956, .T. ) ;
#10983=VERTEX_POINT ( 'NONE', #17297 ) ;
#10997=COLOUR_RGB ( '', 0.72549020, 0.75294118, 0.79215686) ;
#11022=ORIENTED_EDGE ( 'NONE', *, *, #19178, .T. ) ;
#11065=ORIENTED_EDGE ( 'NONE', *, *, #17288, .F. ) ;
#11082=DIRECTION ( 'NONE',  ( 1.000000000000000000, 1.836909530733573776E-16, 0.000000000000000000 ) ) ;
#11086=ORIENTED_EDGE ( 'NONE', *, *, #9023, .F. ) ;
#11099=LINE ( 'NONE', #19152, #16614 ) ;
#11103=DIRECTION ( 'NONE',  ( 0.000000000000000000, 0.000000000000000000, 1.000000000000000000 ) ) ;
#11105=DIRECTION ( 'NONE',  ( 1.000000000000000000, 1.836909530733573776E-16, 0.000000000000000000 ) ) ;
#11112=CARTESIAN_POINT ( 'NONE',  ( 6.679999999999998828, 7.059243326609123303E-15, 0.000000000000000000 ) ) ;
#11126=CARTESIAN_POINT ( 'NONE',  ( 6.232799999999998342, 10.79377999999999993, 0.000000000000000000 ) ) ;
#11135=EDGE_CURVE ( 'NONE', #764, #8758, #20783, .T. ) ;
#11155=APPLICATION_CONTEXT ( 'automotive_design' ) ;
#11202=ORIENTED_EDGE ( 'NONE', *, *, #13366, .T. ) ;
#11234=CARTESIAN_POINT ( 'NONE',  ( -6.165580000000000283, 9.267171751443833528E-16, -7.567219999999999835 ) ) ;
#11259=AXIS2_PLACEMENT_3D ( 'NONE', #4008, #10812, #18647 ) ;
#11327=DIRECTION ( 'NONE',  ( -1.508455196501572169E-16, 1.000000000000000000, 0.000000000000000000 ) ) ;
#11347=SHAPE_REPRESENTATION_RELATIONSHIP ( 'NONE' , 'NONE' ,  #20346, #6131 ) ;
#11364=FACE_OUTER_BOUND ( 'NONE', #18819, .T. ) ;
#11398=SURFACE_STYLE_FILL_AREA ( #1755 ) ;
#11440=ORIENTED_EDGE ( 'NONE', *, *, #6122, .T. ) ;
#11473=ORIENTED_EDGE ( 'NONE', *, *, #5336, .F. ) ;
#11535=ADVANCED_FACE ( 'NONE', ( #1461 ), #3588, .T. ) ;
#11569=DIRECTION ( 'NONE',  ( -1.000000000000000000, -0.000000000000000000, -0.000000000000000000 ) ) ;
#11585=AXIS2_PLACEMENT_3D ( 'NONE', #11659, #8780, #13255 ) ;
#11600=PRESENTATION_STYLE_ASSIGNMENT (( #3434 ) ) ;
#11604=DIRECTION ( 'NONE',  ( 0.000000000000000000, 1.000000000000000000, 0.000000000000000000 ) ) ;
#11631=CYLINDRICAL_SURFACE ( 'NONE', #11736, 10.85999999999999410 ) ;
#11637=VERTEX_POINT ( 'NONE', #14797 ) ;
#11638=DIRECTION ( 'NONE',  ( 0.000000000000000000, 0.000000000000000000, 1.000000000000000000 ) ) ;
#11659=CARTESIAN_POINT ( 'NONE',  ( 6.999999999999999112, 7.118024431592597790E-15, 0.000000000000000000 ) ) ;
#11669=ORIENTED_EDGE ( 'NONE', *, *, #12307, .T. ) ;
#11670=( GEOMETRIC_REPRESENTATION_CONTEXT ( 3 ) GLOBAL_UNCERTAINTY_ASSIGNED_CONTEXT ( ( #5384 ) ) GLOBAL_UNIT_ASSIGNED_CONTEXT ( ( #6360, #4567, #6453 ) ) REPRESENTATION_CONTEXT ( 'NONE', 'WORKASPACE' ) );
#11736=AXIS2_PLACEMENT_3D ( 'NONE', #3274, #19678, #3465 ) ;
#11751=ORIENTED_EDGE ( 'NONE', *, *, #6195, .T. ) ;
#11793=EDGE_LOOP ( 'NONE', ( #6821, #19636 ) ) ;
#11817=EDGE_CURVE ( 'NONE', #2521, #8637, #6645, .T. ) ;
#11932=ORIENTED_EDGE ( 'NONE', *, *, #17740, .T. ) ;
#11940=AXIS2_PLACEMENT_3D ( 'NONE', #3454, #13217, #4952 ) ;
#11975=DIRECTION ( 'NONE',  ( -1.000000000000000000, 0.000000000000000000, 0.000000000000000000 ) ) ;
#11985=DIRECTION ( 'NONE',  ( -1.000000000000000000, -0.000000000000000000, -0.000000000000000000 ) ) ;
#12032=VERTEX_POINT ( 'NONE', #9584 ) ;
#12035=ORIENTED_EDGE ( 'NONE', *, *, #18020, .F. ) ;
#12036=CARTESIAN_POINT ( 'NONE',  ( 6.999999999999997335, 11.17999999999999972, 0.000000000000000000 ) ) ;
#12059=ORIENTED_EDGE ( 'NONE', *, *, #5336, .T. ) ;
#12096=ORIENTED_EDGE ( 'NONE', *, *, #19713, .T. ) ;
#12157=ORIENTED_EDGE ( 'NONE', *, *, #10272, .T. ) ;
#12170=AXIS2_PLACEMENT_3D ( 'NONE', #15331, #819, #20296 ) ;
#12179=LINE ( 'NONE', #14102, #7524 ) ;
#12189=EDGE_CURVE ( 'NONE', #14005, #18991, #6231, .T. ) ;
#12218=CARTESIAN_POINT ( 'NONE',  ( -6.232800000000000118, 1.325911618322048272E-15, -10.79377999999999993 ) ) ;
#12242=CIRCLE ( 'NONE', #7497, 10.52399999999999380 ) ;
#12260=DIRECTION ( 'NONE',  ( -1.597351267013635531E-16, 1.000000000000000000, 0.000000000000000000 ) ) ;
#12261=CARTESIAN_POINT ( 'NONE',  ( 6.232799999999998342, 9.267171751443831555E-16, -7.567219999999999835 ) ) ;
#12281=CARTESIAN_POINT ( 'NONE',  ( 7.000000000000000000, 11.17999999999999972, 0.000000000000000000 ) ) ;
#12307=EDGE_CURVE ( 'NONE', #1037, #12032, #17412, .T. ) ;
#12326=CARTESIAN_POINT ( 'NONE',  ( 6.680000000000000604, -11.49999999999998757, 1.408343819019455584E-15 ) ) ;
#12362=EDGE_CURVE ( 'NONE', #17067, #16258, #151, .T. ) ;
#12426=ORIENTED_EDGE ( 'NONE', *, *, #19628, .F. ) ;
#12433=CARTESIAN_POINT ( 'NONE',  ( -31.75000000000000000, 10.52399999999999558, 0.000000000000000000 ) ) ;
#12439=ORIENTED_EDGE ( 'NONE', *, *, #11817, .F. ) ;
#12461=AXIS2_PLACEMENT_3D ( 'NONE', #19474, #3361, #185 ) ;
#12486=ORIENTED_EDGE ( 'NONE', *, *, #11817, .T. ) ;
#12527=CARTESIAN_POINT ( 'NONE',  ( -6.165580000000000283, 0.000000000000000000, 7.567219999999999835 ) ) ;
#12563=TOROIDAL_SURFACE ( 'NONE', #16593, 10.79377999999999993, 0.06721999999999934972 ) ;
#12565=AXIS2_PLACEMENT_3D ( 'NONE', #12622, #9120, #4240 ) ;
#12579=TOROIDAL_SURFACE ( 'NONE', #15946, 7.567219999999999835, 0.06721999999999977993 ) ;
#12617=AXIS2_PLACEMENT_3D ( 'NONE', #11126, #4971, #93 ) ;
#12622=CARTESIAN_POINT ( 'NONE',  ( 6.679999999999998828, 7.059243326609123303E-15, 0.000000000000000000 ) ) ;
#12630=( NAMED_UNIT ( * ) SI_UNIT ( $, .STERADIAN. ) SOLID_ANGLE_UNIT ( ) );
#12634=EDGE_CURVE ( 'NONE', #10983, #16643, #2862, .T. ) ;
#12674=DIRECTION ( 'NONE',  ( 1.000000000000000000, 1.836909530733573776E-16, 0.000000000000000000 ) ) ;
#12686=AXIS2_PLACEMENT_3D ( 'NONE', #1218, #1326, #5967 ) ;
#12700=FACE_OUTER_BOUND ( 'NONE', #8514, .T. ) ;
#12704=CARTESIAN_POINT ( 'NONE',  ( -6.999999999999995559, 4.546351088565595293E-15, 0.000000000000000000 ) ) ;
#12710=DIRECTION ( 'NONE',  ( 0.000000000000000000, 0.000000000000000000, 1.000000000000000000 ) ) ;
#12721=DIRECTION ( 'NONE',  ( 1.000000000000000000, 1.836909530733573776E-16, 0.000000000000000000 ) ) ;
#12745=DIRECTION ( 'NONE',  ( -1.000000000000000000, -0.000000000000000000, -0.000000000000000000 ) ) ;
#12748=DIRECTION ( 'NONE',  ( 1.000000000000000000, 1.836909530733573776E-16, 0.000000000000000000 ) ) ;
#12760=EDGE_LOOP ( 'NONE', ( #4584, #11022, #6778, #6915 ) ) ;
#12780=DIRECTION ( 'NONE',  ( 0.000000000000000000, 0.000000000000000000, -1.000000000000000000 ) ) ;
#12796=EDGE_CURVE ( 'NONE', #11637, #19132, #7699, .T. ) ;
#12852=ORIENTED_EDGE ( 'NONE', *, *, #13134, .T. ) ;
#12856=ORIENTED_EDGE ( 'NONE', *, *, #1346, .T. ) ;
#12937=DIRECTION ( 'NONE',  ( 0.000000000000000000, -1.224646799147354686E-16, 1.000000000000000000 ) ) ;
#13010=ORIENTED_EDGE ( 'NONE', *, *, #10958, .T. ) ;
#13068=DIRECTION ( 'NONE',  ( 0.000000000000000000, 0.000000000000000000, 1.000000000000000000 ) ) ;
#13086=CARTESIAN_POINT ( 'NONE',  ( 6.232799999999996565, 0.000000000000000000, 10.79377999999999993 ) ) ;
#13134=EDGE_CURVE ( 'NONE', #4444, #12032, #1150, .T. ) ;
#13162=VERTEX_POINT ( 'NONE', #12261 ) ;
#13217=DIRECTION ( 'NONE',  ( 1.000000000000000000, 1.836909530733573776E-16, 0.000000000000000000 ) ) ;
#13230=ORIENTED_EDGE ( 'NONE', *, *, #292, .F. ) ;
#13236=ORIENTED_EDGE ( 'NONE', *, *, #4792, .T. ) ;
#13255=DIRECTION ( 'NONE',  ( -1.551631016079434906E-16, 1.000000000000000000, 0.000000000000000000 ) ) ;
#13281=FACE_OUTER_BOUND ( 'NONE', #12760, .T. ) ;
#13335=FACE_OUTER_BOUND ( 'NONE', #5852, .T. ) ;
#13337=ADVANCED_FACE ( 'NONE', ( #12700 ), #14103, .T. ) ;
#13353=DIRECTION ( 'NONE',  ( 0.000000000000000000, 0.000000000000000000, -1.000000000000000000 ) ) ;
#13366=EDGE_CURVE ( 'NONE', #18697, #15776, #5325, .T. ) ;
#13373=FACE_OUTER_BOUND ( 'NONE', #4465, .T. ) ;
#13380=PRODUCT_DEFINITION ( 'UNKNOWN', '', #18118, #20001 ) ;
#13382=CIRCLE ( 'NONE', #5927, 0.06721999999999977993 ) ;
#13414=( NAMED_UNIT ( * ) SI_UNIT ( $, .STERADIAN. ) SOLID_ANGLE_UNIT ( ) );
#13436=AXIS2_PLACEMENT_3D ( 'NONE', #2415, #8876, #7285 ) ;
#13462=UNCERTAINTY_MEASURE_WITH_UNIT (LENGTH_MEASURE( 1.000000000000000082E-05 ), #3645, 'distance_accuracy_value', 'NONE');
#13463=DIRECTION ( 'NONE',  ( -1.551631016079434906E-16, 1.000000000000000000, 0.000000000000000000 ) ) ;
#13467=AXIS2_PLACEMENT_3D ( 'NONE', #7148, #20080, #5559 ) ;
#13515=VERTEX_POINT ( 'NONE', #12218 ) ;
#13567=DIRECTION ( 'NONE',  ( 0.000000000000000000, 0.000000000000000000, -1.000000000000000000 ) ) ;
#13574=VECTOR ( 'NONE', #665, 1000.000000000000000 ) ;
#13620=ORIENTED_EDGE ( 'NONE', *, *, #17288, .T. ) ;
#13628=EDGE_CURVE ( 'NONE', #10742, #9288, #1908, .T. ) ;
#13647=EDGE_CURVE ( 'NONE', #17067, #5518, #10840, .T. ) ;
#13673=ORIENTED_EDGE ( 'NONE', *, *, #18020, .T. ) ;
#13698=CARTESIAN_POINT ( 'NONE',  ( -31.75000000000000000, 0.000000000000000000, 0.000000000000000000 ) ) ;
#13701=DIRECTION ( 'NONE',  ( -1.000000000000000000, -0.000000000000000000, -0.000000000000000000 ) ) ;
#13710=CIRCLE ( 'NONE', #20465, 11.17999999999999261 ) ;
#13715=DIRECTION ( 'NONE',  ( 1.000000000000000000, 1.836909530733573776E-16, 0.000000000000000000 ) ) ;
#13743=EDGE_CURVE ( 'NONE', #12032, #1037, #4622, .T. ) ;
#13873=ADVANCED_FACE ( 'NONE', ( #11364 ), #9968, .F. ) ;
#13892=ADVANCED_FACE ( 'NONE', ( #13373 ), #4967, .T. ) ;
#13968=AXIS2_PLACEMENT_3D ( 'NONE', #629, #2210, #18318 ) ;
#13991=CARTESIAN_POINT ( 'NONE',  ( 6.680000000000001492, -11.17999999999998550, 1.369155121446739974E-15 ) ) ;
#14005=VERTEX_POINT ( 'NONE', #18561 ) ;
#14011=CIRCLE ( 'NONE', #2157, 0.06721999999999977993 ) ;
#14024=VERTEX_POINT ( 'NONE', #2757 ) ;
#14053=EDGE_LOOP ( 'NONE', ( #1171, #7520 ) ) ;
#14055=DIRECTION ( 'NONE',  ( -1.648349939164583742E-16, 1.000000000000000000, 0.000000000000000000 ) ) ;
#14074=DIRECTION ( 'NONE',  ( -1.000000000000000000, -0.000000000000000000, -0.000000000000000000 ) ) ;
#14078=CARTESIAN_POINT ( 'NONE',  ( 6.359999999999997655, 7.000462221625649605E-15, 0.000000000000000000 ) ) ;
#14096=CIRCLE ( 'NONE', #6677, 10.85999999999999410 ) ;
#14102=CARTESIAN_POINT ( 'NONE',  ( -31.75000000000000000, -11.49999999999999467, 1.408343819019455584E-15 ) ) ;
#14103=TOROIDAL_SURFACE ( 'NONE', #19549, 7.567219999999999835, 0.06721999999999977993 ) ;
#14113=EDGE_LOOP ( 'NONE', ( #351, #12426, #19889, #1988 ) ) ;
#14117=COLOUR_RGB ( '', 0.72549020, 0.75294118, 0.79215686) ;
#14157=FACE_BOUND ( 'NONE', #1814, .T. ) ;
#14161=FACE_OUTER_BOUND ( 'NONE', #19306, .T. ) ;
#14179=FACE_OUTER_BOUND ( 'NONE', #6297, .T. ) ;
#14209=ORIENTED_EDGE ( 'NONE', *, *, #292, .T. ) ;
#14286=ORIENTED_EDGE ( 'NONE', *, *, #12634, .F. ) ;
#14288=CARTESIAN_POINT ( 'NONE',  ( -31.75000000000000000, 0.000000000000000000, 0.000000000000000000 ) ) ;
#14314=DIRECTION ( 'NONE',  ( 0.000000000000000000, 0.000000000000000000, -1.000000000000000000 ) ) ;
#14322=CIRCLE ( 'NONE', #18763, 10.79377999999999993 ) ;
#14344=CIRCLE ( 'NONE', #6201, 10.85999999999999410 ) ;
#14345=CARTESIAN_POINT ( 'NONE',  ( -6.359999999999995879, -10.52399999999999025, 1.288818291422673979E-15 ) ) ;
#14350=ADVANCED_FACE ( 'NONE', ( #9509, #14400 ), #7922, .T. ) ;
#14365=FACE_OUTER_BOUND ( 'NONE', #17321, .T. ) ;
#14376=EDGE_CURVE ( 'NONE', #9288, #10742, #19079, .T. ) ;
#14386=DIRECTION ( 'NONE',  ( -1.648349939164583742E-16, 1.000000000000000000, 0.000000000000000000 ) ) ;
#14400=FACE_BOUND ( 'NONE', #7034, .T. ) ;
#14403=ADVANCED_FACE ( 'NONE', ( #14157, #14365 ), #3014, .F. ) ;
#14406=FACE_OUTER_BOUND ( 'NONE', #6441, .T. ) ;
#14430=CIRCLE ( 'NONE', #10702, 10.52399999999999380 ) ;
#14504=DIRECTION ( 'NONE',  ( 0.000000000000000000, -1.000000000000000000, 1.224646799147355426E-16 ) ) ;
#14534=FILL_AREA_STYLE ('',( #1508 ) ) ;
#14567=CARTESIAN_POINT ( 'NONE',  ( -6.177131623262581250, 10.85999999999999410, 0.000000000000000000 ) ) ;
#14575=ORIENTED_EDGE ( 'NONE', *, *, #3388, .T. ) ;
#14635=VERTEX_POINT ( 'NONE', #19736 ) ;
#14650=TOROIDAL_SURFACE ( 'NONE', #18706, 11.17999999999999261, 0.3200000000000008393 ) ;
#14651=AXIS2_PLACEMENT_3D ( 'NONE', #12704, #11105, #17578 ) ;
#14670=VERTEX_POINT ( 'NONE', #14567 ) ;
#14688=FACE_OUTER_BOUND ( 'NONE', #3049, .T. ) ;
#14697=AXIS2_PLACEMENT_3D ( 'NONE', #41, #13701, #2458 ) ;
#14712=AXIS2_PLACEMENT_3D ( 'NONE', #15368, #13567, #11975 ) ;
#14729=ORIENTED_EDGE ( 'NONE', *, *, #3350, .T. ) ;
#14739=CARTESIAN_POINT ( 'NONE',  ( -6.999999999999993783, -11.17999999999998906, 1.388749470233097779E-15 ) ) ;
#14741=ORIENTED_EDGE ( 'NONE', *, *, #10414, .F. ) ;
#14757=ORIENTED_EDGE ( 'NONE', *, *, #19033, .F. ) ;
#14769=CARTESIAN_POINT ( 'NONE',  ( -6.232800000000000118, 0.000000000000000000, 0.000000000000000000 ) ) ;
#14797=CARTESIAN_POINT ( 'NONE',  ( -6.177131623262581250, -10.85999999999999410, 1.329966423874025547E-15 ) ) ;
#14798=EDGE_CURVE ( 'NONE', #10258, #10665, #14011, .T. ) ;
#14822=DIRECTION ( 'NONE',  ( -1.836909530733573776E-16, 1.000000000000000000, 0.000000000000000000 ) ) ;
#14827=FACE_OUTER_BOUND ( 'NONE', #10391, .T. ) ;
#14889=CARTESIAN_POINT ( 'NONE',  ( -6.680000000000000604, 11.50000000000000000, 0.000000000000000000 ) ) ;
#14922=ORIENTED_EDGE ( 'NONE', *, *, #6195, .F. ) ;
#14959=AXIS2_PLACEMENT_3D ( 'NONE', #9341, #12745, #7751 ) ;
#15001=DIRECTION ( 'NONE',  ( -1.508455196501572169E-16, 1.000000000000000000, 0.000000000000000000 ) ) ;
#15003=AXIS2_PLACEMENT_3D ( 'NONE', #1334, #20808, #12780 ) ;
#15005=ORIENTED_EDGE ( 'NONE', *, *, #16443, .T. ) ;
#15057=ORIENTED_EDGE ( 'NONE', *, *, #17626, .T. ) ;
#15058=ADVANCED_FACE ( 'NONE', ( #7874 ), #2898, .F. ) ;
#15155=CIRCLE ( 'NONE', #6023, 11.49999999999999467 ) ;
#15325=CARTESIAN_POINT ( 'NONE',  ( -25.39999999999999858, 0.000000000000000000, 0.000000000000000000 ) ) ;
#15331=CARTESIAN_POINT ( 'NONE',  ( 6.177131623262577698, 0.000000000000000000, 0.000000000000000000 ) ) ;
#15345=ORIENTED_EDGE ( 'NONE', *, *, #10958, .F. ) ;
#15347=ORIENTED_EDGE ( 'NONE', *, *, #6526, .T. ) ;
#15365=ORIENTED_EDGE ( 'NONE', *, *, #14376, .T. ) ;
#15368=CARTESIAN_POINT ( 'NONE',  ( -6.679999999999999716, 11.17999999999999972, 0.000000000000000000 ) ) ;
#15474=ORIENTED_EDGE ( 'NONE', *, *, #19033, .T. ) ;
#15477=DIRECTION ( 'NONE',  ( 1.000000000000000000, 0.000000000000000000, 0.000000000000000000 ) ) ;
#15499=DIRECTION ( 'NONE',  ( -1.000000000000000000, -0.000000000000000000, -0.000000000000000000 ) ) ;
#15625=AXIS2_PLACEMENT_3D ( 'NONE', #13698, #16455, #18464 ) ;
#15749=ORIENTED_EDGE ( 'NONE', *, *, #1740, .T. ) ;
#15775=FACE_BOUND ( 'NONE', #14053, .T. ) ;
#15776=VERTEX_POINT ( 'NONE', #17920 ) ;
#15795=TOROIDAL_SURFACE ( 'NONE', #9034, 11.17999999999999439, 0.3200000000000012834 ) ;
#15842=VERTEX_POINT ( 'NONE', #3477 ) ;
#15891=PLANE ( 'NONE',  #12617 ) ;
#15914=ORIENTED_EDGE ( 'NONE', *, *, #10331, .F. ) ;
#15929=DIRECTION ( 'NONE',  ( -0.000000000000000000, 1.000000000000000000, 1.224646799147353207E-16 ) ) ;
#15944=ADVANCED_FACE ( 'NONE', ( #6029, #15775 ), #9107, .T. ) ;
#15946=AXIS2_PLACEMENT_3D ( 'NONE', #3805, #10290, #16750 ) ;
#15960=AXIS2_PLACEMENT_3D ( 'NONE', #14288, #6017, #4214 ) ;
#15961=CARTESIAN_POINT ( 'NONE',  ( 6.165580000000000283, 0.000000000000000000, 0.000000000000000000 ) ) ;
#15966=CARTESIAN_POINT ( 'NONE',  ( -6.165580000000000283, 0.000000000000000000, 0.000000000000000000 ) ) ;
#15995=CIRCLE ( 'NONE', #6838, 10.85999999999999233 ) ;
#16086=DIRECTION ( 'NONE',  ( -1.836909530733573776E-16, 1.000000000000000000, 0.000000000000000000 ) ) ;
#16110=CARTESIAN_POINT ( 'NONE',  ( -25.39999999999999858, 0.000000000000000000, 7.500000000000000000 ) ) ;
#16191=CARTESIAN_POINT ( 'NONE',  ( -6.360000000000001208, 10.85999999999999943, 0.000000000000000000 ) ) ;
#16213=VERTEX_POINT ( 'NONE', #10561 ) ;
#16258=VERTEX_POINT ( 'NONE', #8754 ) ;
#16269=DIRECTION ( 'NONE',  ( -1.000000000000000000, -0.000000000000000000, -0.000000000000000000 ) ) ;
#16312=CIRCLE ( 'NONE', #19354, 7.567219999999999835 ) ;
#16320=ADVANCED_FACE ( 'NONE', ( #14179 ), #1462, .T. ) ;
#16370=SURFACE_SIDE_STYLE ('',( #11398 ) ) ;
#16372=DIRECTION ( 'NONE',  ( 0.000000000000000000, 0.000000000000000000, 1.000000000000000000 ) ) ;
#16388=ORIENTED_EDGE ( 'NONE', *, *, #17020, .T. ) ;
#16413=CARTESIAN_POINT ( 'NONE',  ( -6.999999999999995559, 4.546351088565595293E-15, 0.000000000000000000 ) ) ;
#16430=ORIENTED_EDGE ( 'NONE', *, *, #4702, .T. ) ;
#16442=EDGE_CURVE ( 'NONE', #7461, #4444, #7926, .T. ) ;
#16443=EDGE_CURVE ( 'NONE', #3991, #4894, #14322, .T. ) ;
#16455=DIRECTION ( 'NONE',  ( 1.000000000000000000, 1.836909530733573776E-16, 0.000000000000000000 ) ) ;
#16460=DIRECTION ( 'NONE',  ( 1.000000000000000000, 1.836909530733573776E-16, 0.000000000000000000 ) ) ;
#16546=ADVANCED_FACE ( 'NONE', ( #14688 ), #12563, .T. ) ;
#16583=ORIENTED_EDGE ( 'NONE', *, *, #7693, .F. ) ;
#16593=AXIS2_PLACEMENT_3D ( 'NONE', #159, #1561, #17968 ) ;
#16602=ORIENTED_EDGE ( 'NONE', *, *, #13647, .T. ) ;
#16607=CARTESIAN_POINT ( 'NONE',  ( -31.75000000000000000, -10.52399999999999558, 1.288818291422673979E-15 ) ) ;
#16614=VECTOR ( 'NONE', #4627, 1000.000000000000000 ) ;
#16616=FACE_BOUND ( 'NONE', #20101, .T. ) ;
#16622=UNCERTAINTY_MEASURE_WITH_UNIT (LENGTH_MEASURE( 1.000000000000000082E-05 ), #20772, 'distance_accuracy_value', 'NONE');
#16623=CARTESIAN_POINT ( 'NONE',  ( -6.177131623262581250, 0.000000000000000000, 10.85999999999999410 ) ) ;
#16643=VERTEX_POINT ( 'NONE', #14889 ) ;
#16652=AXIS2_PLACEMENT_3D ( 'NONE', #18237, #6990, #19919 ) ;
#16663=ORIENTED_EDGE ( 'NONE', *, *, #18800, .F. ) ;
#16665=DIRECTION ( 'NONE',  ( 0.000000000000000000, 0.000000000000000000, 1.000000000000000000 ) ) ;
#16670=AXIS2_PLACEMENT_3D ( 'NONE', #1592, #6543, #3363 ) ;
#16721=FACE_OUTER_BOUND ( 'NONE', #1562, .T. ) ;
#16750=DIRECTION ( 'NONE',  ( 0.000000000000000000, 0.000000000000000000, 1.000000000000000000 ) ) ;
#16839=DIRECTION ( 'NONE',  ( 1.000000000000000000, 1.836909530733573776E-16, 0.000000000000000000 ) ) ;
#16849=CYLINDRICAL_SURFACE ( 'NONE', #2626, 11.49999999999999467 ) ;
#16914=DIRECTION ( 'NONE',  ( -1.000000000000000000, -0.000000000000000000, -0.000000000000000000 ) ) ;
#16953=CARTESIAN_POINT ( 'NONE',  ( 6.165580000000000283, 0.000000000000000000, 0.000000000000000000 ) ) ;
#16991=ADVANCED_FACE ( 'NONE', ( #9783, #3010 ), #17854, .T. ) ;
#17020=EDGE_CURVE ( 'NONE', #10665, #13515, #17630, .T. ) ;
#17067=VERTEX_POINT ( 'NONE', #6902 ) ;
#17121=DIRECTION ( 'NONE',  ( -1.648349939164583742E-16, 1.000000000000000000, 0.000000000000000000 ) ) ;
#17274=DIRECTION ( 'NONE',  ( 0.000000000000000000, -1.000000000000000000, 1.224646799147355426E-16 ) ) ;
#17288=EDGE_CURVE ( 'NONE', #10258, #11637, #3108, .T. ) ;
#17297=CARTESIAN_POINT ( 'NONE',  ( -6.999999999999997335, 11.17999999999999972, 0.000000000000000000 ) ) ;
#17303=CARTESIAN_POINT ( 'NONE',  ( 6.177131623262577698, 0.000000000000000000, 0.000000000000000000 ) ) ;
#17310=DIRECTION ( 'NONE',  ( 0.000000000000000000, 0.000000000000000000, 1.000000000000000000 ) ) ;
#17321=EDGE_LOOP ( 'NONE', ( #16388, #12096 ) ) ;
#17327=ADVANCED_FACE ( 'NONE', ( #2875 ), #5121, .T. ) ;
#17396=AXIS2_PLACEMENT_3D ( 'NONE', #6585, #11569, #13068 ) ;
#17412=CIRCLE ( 'NONE', #14697, 7.500000000000000000 ) ;
#17462=DIRECTION ( 'NONE',  ( 0.000000000000000000, 0.000000000000000000, 1.000000000000000000 ) ) ;
#17492=CARTESIAN_POINT ( 'NONE',  ( -6.177131623262581250, 0.000000000000000000, 0.000000000000000000 ) ) ;
#17528=ORIENTED_EDGE ( 'NONE', *, *, #2200, .F. ) ;
#17533=ORIENTED_EDGE ( 'NONE', *, *, #1989, .F. ) ;
#17578=DIRECTION ( 'NONE',  ( -1.551631016079434660E-16, 1.000000000000000000, 0.000000000000000000 ) ) ;
#17591=DIRECTION ( 'NONE',  ( -1.836909530733573776E-16, 1.000000000000000000, 0.000000000000000000 ) ) ;
#17626=EDGE_CURVE ( 'NONE', #18991, #14005, #16312, .T. ) ;
#17630=CIRCLE ( 'NONE', #12, 10.79377999999999993 ) ;
#17657=DIRECTION ( 'NONE',  ( 0.000000000000000000, 0.000000000000000000, -1.000000000000000000 ) ) ;
#17701=EDGE_LOOP ( 'NONE', ( #6411, #9304, #13236, #11669 ) ) ;
#17709=DIRECTION ( 'NONE',  ( -0.000000000000000000, 1.000000000000000000, 1.224646799147353207E-16 ) ) ;
#17734=ORIENTED_EDGE ( 'NONE', *, *, #10637, .T. ) ;
#17740=EDGE_CURVE ( 'NONE', #764, #18535, #19951, .T. ) ;
#17757=DIRECTION ( 'NONE',  ( -1.597351267013635284E-16, 1.000000000000000000, 0.000000000000000000 ) ) ;
#17786=DIRECTION ( 'NONE',  ( 1.000000000000000000, 1.836909530733573776E-16, 0.000000000000000000 ) ) ;
#17790=CARTESIAN_POINT ( 'NONE',  ( -31.75000000000000000, 0.000000000000000000, 0.000000000000000000 ) ) ;
#17807=ORIENTED_EDGE ( 'NONE', *, *, #17626, .F. ) ;
#17818=SURFACE_STYLE_FILL_AREA ( #14534 ) ;
#17820=ADVANCED_FACE ( 'NONE', ( #5130 ), #5345, .F. ) ;
#17840=CARTESIAN_POINT ( 'NONE',  ( -31.75000000000000000, 0.000000000000000000, 0.000000000000000000 ) ) ;
#17853=AXIS2_PLACEMENT_3D ( 'NONE', #19398, #4991, #19704 ) ;
#17854=PLANE ( 'NONE',  #5765 ) ;
#17857=ORIENTED_EDGE ( 'NONE', *, *, #14798, .F. ) ;
#17890=ORIENTED_EDGE ( 'NONE', *, *, #5532, .T. ) ;
#17920=CARTESIAN_POINT ( 'NONE',  ( -6.679999999999997051, -11.49999999999998934, 1.408343819019455584E-15 ) ) ;
#17968=DIRECTION ( 'NONE',  ( 0.000000000000000000, 0.000000000000000000, 1.000000000000000000 ) ) ;
#18020=EDGE_CURVE ( 'NONE', #19132, #13515, #8577, .T. ) ;
#18033=ORIENTED_EDGE ( 'NONE', *, *, #10637, .F. ) ;
#18045=CARTESIAN_POINT ( 'NONE',  ( 6.999999999999997335, 10.52400000000000091, 0.000000000000000000 ) ) ;
#18052=ORIENTED_EDGE ( 'NONE', *, *, #1989, .T. ) ;
#18053=CYLINDRICAL_SURFACE ( 'NONE', #15625, 11.49999999999999467 ) ;
#18055=ORIENTED_EDGE ( 'NONE', *, *, #17020, .F. ) ;
#18094=SHAPE_DEFINITION_REPRESENTATION ( #352, #20346 ) ;
#18118=PRODUCT_DEFINITION_FORMATION_WITH_SPECIFIED_SOURCE ( 'ANY', '', #8811, .NOT_KNOWN. ) ;
#18152=CIRCLE ( 'NONE', #6304, 11.49999999999999467 ) ;
#18157=CARTESIAN_POINT ( 'NONE',  ( -6.679999999999997939, 5.204170427930421283E-15, 0.000000000000000000 ) ) ;
#18177=CARTESIAN_POINT ( 'NONE',  ( 6.165579999999999394, 0.000000000000000000, 10.79377999999999993 ) ) ;
#18186=LINE ( 'NONE', #489, #20513 ) ;
#18192=CARTESIAN_POINT ( 'NONE',  ( 6.359999999999997655, 7.000462221625649605E-15, 0.000000000000000000 ) ) ;
#18237=CARTESIAN_POINT ( 'NONE',  ( 6.679999999999998828, 11.17999999999999972, 0.000000000000000000 ) ) ;
#18279=CARTESIAN_POINT ( 'NONE',  ( -6.359999999999997655, 4.663913298532544267E-15, 0.000000000000000000 ) ) ;
#18314=ORIENTED_EDGE ( 'NONE', *, *, #5893, .T. ) ;
#18318=DIRECTION ( 'NONE',  ( 1.836909530733573776E-16, -1.000000000000000000, 0.000000000000000000 ) ) ;
#18324=APPLICATION_CONTEXT ( 'automotive_design' ) ;
#18374=CARTESIAN_POINT ( 'NONE',  ( 6.680000000000000604, 6.938893903907228378E-15, 0.000000000000000000 ) ) ;
#18464=DIRECTION ( 'NONE',  ( 0.000000000000000000, 1.000000000000000000, 0.000000000000000000 ) ) ;
#18465=CIRCLE ( 'NONE', #6287, 7.567219999999999835 ) ;
#18496=DIRECTION ( 'NONE',  ( 0.000000000000000000, 0.000000000000000000, 1.000000000000000000 ) ) ;
#18508=AXIS2_PLACEMENT_3D ( 'NONE', #18279, #10443, #5442 ) ;
#18511=AXIS2_PLACEMENT_3D ( 'NONE', #7549, #9459, #17310 ) ;
#18535=VERTEX_POINT ( 'NONE', #20576 ) ;
#18541=CARTESIAN_POINT ( 'NONE',  ( 6.232799999999998342, 0.000000000000000000, 7.567219999999999835 ) ) ;
#18561=CARTESIAN_POINT ( 'NONE',  ( -6.232800000000000118, 0.000000000000000000, 7.567219999999999835 ) ) ;
#18570=CARTESIAN_POINT ( 'NONE',  ( -6.679999999999997939, 5.204170427930421283E-15, 0.000000000000000000 ) ) ;
#18573=DIRECTION ( 'NONE',  ( 0.000000000000000000, -1.000000000000000000, 0.000000000000000000 ) ) ;
#18647=DIRECTION ( 'NONE',  ( -1.597351267013635284E-16, 1.000000000000000000, 0.000000000000000000 ) ) ;
#18659=DIRECTION ( 'NONE',  ( 0.000000000000000000, 0.000000000000000000, 1.000000000000000000 ) ) ;
#18697=VERTEX_POINT ( 'NONE', #14739 ) ;
#18706=AXIS2_PLACEMENT_3D ( 'NONE', #3460, #8345, #14822 ) ;
#18715=EDGE_LOOP ( 'NONE', ( #16430, #15474, #9938, #7970 ) ) ;
#18716=FACE_OUTER_BOUND ( 'NONE', #7128, .T. ) ;
#18727=AXIS2_PLACEMENT_3D ( 'NONE', #3353, #6328, #9620 ) ;
#18763=AXIS2_PLACEMENT_3D ( 'NONE', #4930, #16269, #16372 ) ;
#18800=EDGE_CURVE ( 'NONE', #14670, #10258, #7346, .T. ) ;
#18819=EDGE_LOOP ( 'NONE', ( #20760, #9243, #6040, #5825, #4270 ) ) ;
#18824=ORIENTED_EDGE ( 'NONE', *, *, #7528, .F. ) ;
#18854=DIRECTION ( 'NONE',  ( -1.508455196501572169E-16, 1.000000000000000000, 0.000000000000000000 ) ) ;
#18934=DIRECTION ( 'NONE',  ( 0.000000000000000000, -1.000000000000000000, 0.000000000000000000 ) ) ;
#18946=ADVANCED_FACE ( 'NONE', ( #2014 ), #16849, .T. ) ;
#18991=VERTEX_POINT ( 'NONE', #4343 ) ;
#19005=DIRECTION ( 'NONE',  ( -1.648349939164583989E-16, 1.000000000000000000, 0.000000000000000000 ) ) ;
#19033=EDGE_CURVE ( 'NONE', #2254, #6330, #4316, .T. ) ;
#19049=DIRECTION ( 'NONE',  ( 1.000000000000000000, 1.836909530733573776E-16, 0.000000000000000000 ) ) ;
#19079=CIRCLE ( 'NONE', #18727, 10.52399999999999380 ) ;
#19086=ORIENTED_EDGE ( 'NONE', *, *, #12796, .T. ) ;
#19093=SURFACE_STYLE_USAGE ( .BOTH. , #7958 ) ;
#19103=DIRECTION ( 'NONE',  ( 0.000000000000000000, 0.000000000000000000, -1.000000000000000000 ) ) ;
#19128=ORIENTED_EDGE ( 'NONE', *, *, #19319, .F. ) ;
#19132=VERTEX_POINT ( 'NONE', #6825 ) ;
#19139=AXIS2_PLACEMENT_3D ( 'NONE', #8112, #9598, #14386 ) ;
#19144=CARTESIAN_POINT ( 'NONE',  ( 6.165580000000000283, 0.000000000000000000, 7.567219999999999835 ) ) ;
#19149=DIRECTION ( 'NONE',  ( -1.000000000000000000, -0.000000000000000000, -0.000000000000000000 ) ) ;
#19152=CARTESIAN_POINT ( 'NONE',  ( -31.75000000000000000, 10.52399999999999380, 0.000000000000000000 ) ) ;
#19160=AXIS2_PLACEMENT_3D ( 'NONE', #12527, #4464, #19103 ) ;
#19178=EDGE_CURVE ( 'NONE', #15776, #16643, #18152, .T. ) ;
#19182=EDGE_LOOP ( 'NONE', ( #6021, #17890 ) ) ;
#19207=EDGE_CURVE ( 'NONE', #16643, #15842, #18186, .T. ) ;
#19247=DIRECTION ( 'NONE',  ( -1.000000000000000000, -0.000000000000000000, -0.000000000000000000 ) ) ;
#19275=ORIENTED_EDGE ( 'NONE', *, *, #6854, .T. ) ;
#19306=EDGE_LOOP ( 'NONE', ( #14729, #11202, #9387, #14286 ) ) ;
#19319=EDGE_CURVE ( 'NONE', #16258, #764, #14096, .T. ) ;
#19354=AXIS2_PLACEMENT_3D ( 'NONE', #6923, #6224, #12710 ) ;
#19398=CARTESIAN_POINT ( 'NONE',  ( -6.177131623262581250, 0.000000000000000000, 0.000000000000000000 ) ) ;
#19402=CARTESIAN_POINT ( 'NONE',  ( -6.165580000000000283, 0.000000000000000000, 7.500000000000000000 ) ) ;
#19410=EDGE_LOOP ( 'NONE', ( #12059, #7775 ) ) ;
#19422=VECTOR ( 'NONE', #10836, 1000.000000000000000 ) ;
#19432=DIRECTION ( 'NONE',  ( -1.000000000000000000, -0.000000000000000000, -0.000000000000000000 ) ) ;
#19448=CARTESIAN_POINT ( 'NONE',  ( 6.165579999999996730, 0.000000000000000000, 0.000000000000000000 ) ) ;
#19461=EDGE_LOOP ( 'NONE', ( #20390, #11440, #1393, #15345 ) ) ;
#19474=CARTESIAN_POINT ( 'NONE',  ( 0.000000000000000000, 0.000000000000000000, 0.000000000000000000 ) ) ;
#19478=FACE_OUTER_BOUND ( 'NONE', #19882, .T. ) ;
#19486=FACE_OUTER_BOUND ( 'NONE', #5826, .T. ) ;
#19494=CARTESIAN_POINT ( 'NONE',  ( -6.177131623262581250, 0.000000000000000000, 0.000000000000000000 ) ) ;
#19516=STYLED_ITEM ( 'NONE', ( #3185 ), #6131 ) ;
#19522=AXIS2_PLACEMENT_3D ( 'NONE', #16953, #7197, #8589 ) ;
#19531=CARTESIAN_POINT ( 'NONE',  ( 6.359999999999999432, 10.52400000000000091, 0.000000000000000000 ) ) ;
#19549=AXIS2_PLACEMENT_3D ( 'NONE', #15966, #9999, #11103 ) ;
#19587=ORIENTED_EDGE ( 'NONE', *, *, #12796, .F. ) ;
#19628=EDGE_CURVE ( 'NONE', #20371, #200, #1919, .T. ) ;
#19636=ORIENTED_EDGE ( 'NONE', *, *, #3388, .F. ) ;
#19639=ORIENTED_EDGE ( 'NONE', *, *, #8157, .T. ) ;
#19651=ADVANCED_FACE ( 'NONE', ( #14161 ), #15795, .T. ) ;
#19678=DIRECTION ( 'NONE',  ( 1.000000000000000000, 1.836909530733573776E-16, 0.000000000000000000 ) ) ;
#19694=FACE_OUTER_BOUND ( 'NONE', #2378, .T. ) ;
#19703=CIRCLE ( 'NONE', #14651, 11.17999999999999439 ) ;
#19704=DIRECTION ( 'NONE',  ( 0.000000000000000000, 0.000000000000000000, -1.000000000000000000 ) ) ;
#19713=EDGE_CURVE ( 'NONE', #13515, #10665, #4959, .T. ) ;
#19736=CARTESIAN_POINT ( 'NONE',  ( 6.359999999999999432, -10.52399999999998670, 1.288818291422673781E-15 ) ) ;
#19757=ORIENTED_EDGE ( 'NONE', *, *, #5069, .F. ) ;
#19818=ADVANCED_FACE ( 'NONE', ( #14827 ), #11631, .F. ) ;
#19835=DIRECTION ( 'NONE',  ( 0.000000000000000000, 0.000000000000000000, 1.000000000000000000 ) ) ;
#19882=EDGE_LOOP ( 'NONE', ( #14757, #15347, #2931, #8924 ) ) ;
#19889=ORIENTED_EDGE ( 'NONE', *, *, #2248, .T. ) ;
#19905=FACE_OUTER_BOUND ( 'NONE', #17701, .T. ) ;
#19919=DIRECTION ( 'NONE',  ( -1.000000000000000000, 0.000000000000000000, 0.000000000000000000 ) ) ;
#19951=CIRCLE ( 'NONE', #12170, 10.85999999999999410 ) ;
#19958=ORIENTED_EDGE ( 'NONE', *, *, #12189, .F. ) ;
#20001=PRODUCT_DEFINITION_CONTEXT ( 'detailed design', #11155, 'design' ) ;
#20058=ORIENTED_EDGE ( 'NONE', *, *, #19713, .F. ) ;
#20080=DIRECTION ( 'NONE',  ( -0.000000000000000000, 1.000000000000000000, 1.224646799147353207E-16 ) ) ;
#20101=EDGE_LOOP ( 'NONE', ( #1453, #15749 ) ) ;
#20114=EDGE_CURVE ( 'NONE', #8758, #5518, #3616, .T. ) ;
#20129=FACE_OUTER_BOUND ( 'NONE', #19461, .T. ) ;
#20263=LINE ( 'NONE', #8722, #13574 ) ;
#20296=DIRECTION ( 'NONE',  ( 0.000000000000000000, 0.000000000000000000, 1.000000000000000000 ) ) ;
#20311=ORIENTED_EDGE ( 'NONE', *, *, #9754, .F. ) ;
#20346=SHAPE_REPRESENTATION ( 'needle roller bearing_nh_iso_ISO 3245 - 1532D - 14,SI,NC,14', ( #12461 ), #2252 ) ;
#20371=VERTEX_POINT ( 'NONE', #6938 ) ;
#20389=CIRCLE ( 'NONE', #11259, 10.85999999999999410 ) ;
#20390=ORIENTED_EDGE ( 'NONE', *, *, #12189, .T. ) ;
#20403=CARTESIAN_POINT ( 'NONE',  ( 6.165579999999999394, 0.000000000000000000, 0.000000000000000000 ) ) ;
#20434=AXIS2_PLACEMENT_3D ( 'NONE', #1430, #7880, #6076 ) ;
#20439=CIRCLE ( 'NONE', #17396, 7.567219999999999835 ) ;
#20465=AXIS2_PLACEMENT_3D ( 'NONE', #6974, #5385, #13463 ) ;
#20513=VECTOR ( 'NONE', #3651, 1000.000000000000000 ) ;
#20576=CARTESIAN_POINT ( 'NONE',  ( 6.177131623262577698, 1.329966423874024758E-15, -10.85999999999999410 ) ) ;
#20606=ORIENTED_EDGE ( 'NONE', *, *, #8157, .F. ) ;
#20619=CARTESIAN_POINT ( 'NONE',  ( -6.165580000000000283, 0.000000000000000000, 0.000000000000000000 ) ) ;
#20633=DIRECTION ( 'NONE',  ( -1.648349939164583989E-16, 1.000000000000000000, 0.000000000000000000 ) ) ;
#20648=AXIS2_PLACEMENT_3D ( 'NONE', #18570, #12721, #17591 ) ;
#20682=CARTESIAN_POINT ( 'NONE',  ( 6.999999999999999112, 7.118024431592597790E-15, 0.000000000000000000 ) ) ;
#20696=AXIS2_PLACEMENT_3D ( 'NONE', #1618, #6262, #9545 ) ;
#20718=DIRECTION ( 'NONE',  ( 0.000000000000000000, 0.000000000000000000, 1.000000000000000000 ) ) ;
#20741=AXIS2_PLACEMENT_3D ( 'NONE', #16191, #17786, #16086 ) ;
#20760=ORIENTED_EDGE ( 'NONE', *, *, #13647, .F. ) ;
#20772=( LENGTH_UNIT ( ) NAMED_UNIT ( * ) SI_UNIT ( .MILLI., .METRE. ) );
#20783=LINE ( 'NONE', #1620, #881 ) ;
#20808=DIRECTION ( 'NONE',  ( 1.000000000000000000, 0.000000000000000000, 0.000000000000000000 ) ) ;
#20877=EDGE_CURVE ( 'NONE', #16643, #15776, #15155, .T. ) ;
#20911=CARTESIAN_POINT ( 'NONE',  ( -6.232800000000000118, 0.000000000000000000, 10.79377999999999993 ) ) ;
ENDSEC;
END-ISO-10303-21;
